ISO-10303-21;
HEADER;
FILE_DESCRIPTION (('STEP AP214'),
    '1' );
FILE_NAME ('Parallelogram front_REAR.step',
    '2026-10-12T23:53:07',
    ( '' ),
    ( '' ),
    'SwSTEP 2.0',
    'SolidWorks 2024',
    '' );
FILE_SCHEMA (( 'AUTOMOTIVE_DESIGN' ));
ENDSEC;

DATA;
#66=ADVANCED_FACE ( 'NONE', ( #33910 ), #4970, .T. ) ;
#101=AXIS2_PLACEMENT_3D ( 'NONE', #14971, #21565, #27524 ) ;
#104=CARTESIAN_POINT ( 'NONE',  ( -0.1710642717957937542, 0.4986889573705819423, 0.1482573527501182542 ) ) ;
#122=CARTESIAN_POINT ( 'NONE',  ( -0.1212602504878775439, -0.5073146173917505442, 0.3032895567580813356 ) ) ;
#129=ADVANCED_FACE ( 'NONE', ( #22978 ), #24068, .T. ) ;
#136=DIRECTION ( 'NONE',  ( 1.000000000000000000, 2.276539994720204558E-15, -1.138269997360102279E-15 ) ) ;
#145=EDGE_LOOP ( 'NONE', ( #25548, #19484 ) ) ;
#187=ADVANCED_FACE ( 'NONE', ( #3432 ), #37791, .T. ) ;
#196=CARTESIAN_POINT ( 'NONE',  ( -1.019575837292305831, -0.04310840302198155199, 0.3750000000000002220 ) ) ;
#203=ORIENTED_EDGE ( 'NONE', *, *, #10449, .T. ) ;
#220=CARTESIAN_POINT ( 'NONE',  ( -0.1172401355130585354, -0.4876450271194930908, 0.3356658914665637816 ) ) ;
#240=ORIENTED_EDGE ( 'NONE', *, *, #36669, .T. ) ;
#312=DIRECTION ( 'NONE',  ( 8.881784197001246407E-16, -2.361472542561082612E-16, 1.000000000000000000 ) ) ;
#315=CARTESIAN_POINT ( 'NONE',  ( -0.1542132178619276262, 0.4779941576916627022, 0.1100664889103354915 ) ) ;
#323=CARTESIAN_POINT ( 'NONE',  ( -0.1553124468364829591, 0.4816356660588166916, 0.3589899338161261499 ) ) ;
#425=CARTESIAN_POINT ( 'NONE',  ( -0.1157263453858495550, -0.4799749855354071837, 0.1178658435936998650 ) ) ;
#515=ORIENTED_EDGE ( 'NONE', *, *, #8471, .T. ) ;
#527=CARTESIAN_POINT ( 'NONE',  ( -0.1566201954065912505, 0.4859225043295721247, 0.1133527062597488727 ) ) ;
#614=B_SPLINE_CURVE_WITH_KNOTS ( 'NONE', 3,
 ( #11813, #21512, #9126, #40607, #122 ),
 .UNSPECIFIED., .F., .F.,
 ( 4, 1, 4 ),
 ( 0.003975523017580721505, 0.004090739973965705316, 0.004205956930350687392 ),
 .UNSPECIFIED. ) ;
#615=CARTESIAN_POINT ( 'NONE',  ( -0.1172150163384020338, -0.4875187859579048211, 0.1204312767266917522 ) ) ;
#636=DIRECTION ( 'NONE',  ( 1.000000000000000000, 1.138269997360102279E-15, -8.537024980200767584E-16 ) ) ;
#643=( BOUNDED_SURFACE ( )  B_SPLINE_SURFACE ( 3, 2, ( 
 ( #31943, #16120, #9724 ),
 ( #35014, #9306, #18989 ),
 ( #12403, #315, #6228 ),
 ( #31522, #527, #31347 ),
 ( #22706, #35237, #15690 ),
 ( #12601, #31731, #15897 ),
 ( #37700, #3334, #13022 ),
 ( #25571, #25780, #38100 ),
 ( #34807, #7038, #6611 ),
 ( #9918, #22489, #2952 ),
 ( #15504, #16316, #22293 ),
 ( #28239, #28852, #12820 ),
 ( #24956, #712, #104 ),
 ( #40582, #21885, #34413 ) ),
 .UNSPECIFIED., .F., .F., .T. ) 
 B_SPLINE_SURFACE_WITH_KNOTS ( ( 4, 2, 2, 2, 2, 2, 4 ),
 ( 3, 3 ),
 ( 0.001271275560265211274, 0.001846161198739981746, 0.002133604017977366873, 0.002421046837214752001, 0.002708489656452137129, 0.002995932475689522256, 0.003570818114164292512 ),
 ( 0.000000000000000000, 1.000000000000000000 ),
 .UNSPECIFIED. ) 
 GEOMETRIC_REPRESENTATION_ITEM ( )  RATIONAL_B_SPLINE_SURFACE ( (
 ( 1.000000000000000000, 0.9128709291753037691, 1.000000000000000000),
 ( 1.000000000000000000, 0.9128716273348949084, 1.000000000000000000),
 ( 1.000000000000000000, 0.9128126260588453889, 1.000000000000000000),
 ( 1.000000000000000000, 0.9126599423562549163, 1.000000000000000000),
 ( 1.000000000000000000, 0.9125975471393394933, 1.000000000000000000),
 ( 1.000000000000000000, 0.9124617177696037196, 1.000000000000000000),
 ( 1.000000000000000000, 0.9123879986972855960, 1.000000000000000000),
 ( 1.000000000000000000, 0.9122366710452365357, 1.000000000000000000),
 ( 1.000000000000000000, 0.9121592624379363246, 1.000000000000000000),
 ( 1.000000000000000000, 0.9120163032376494838, 1.000000000000000000),
 ( 1.000000000000000000, 0.9119498413173655615, 1.000000000000000000),
 ( 1.000000000000000000, 0.9117793221106540447, 1.000000000000000000),
 ( 1.000000000000000000, 0.9117124009643396976, 1.000000000000000000),
 ( 1.000000000000000000, 0.9117127123830720548, 1.000000000000000000) ) ) 
 REPRESENTATION_ITEM ( '' )  SURFACE ( )  );
#664=ORIENTED_EDGE ( 'NONE', *, *, #20227, .F. ) ;
#683=DIRECTION ( 'NONE',  ( 1.000000000000000000, 4.553079989440409115E-15, -1.138269997360102279E-15 ) ) ;
#712=CARTESIAN_POINT ( 'NONE',  ( -0.1642263572652833681, 0.5103503757440389643, 0.1470331037154066212 ) ) ;
#773=CARTESIAN_POINT ( 'NONE',  ( -2.070754768975509919, -0.09959325338431655739, 0.1178658435937004478 ) ) ;
#797=CARTESIAN_POINT ( 'NONE',  ( -0.1731185243557762099, 0.5373335498847187086, 0.3599999999999999867 ) ) ;
#802=DIRECTION ( 'NONE',  ( 8.326672684688655318E-16, -2.361472542561083598E-16, 1.000000000000000000 ) ) ;
#853=DIRECTION ( 'NONE',  ( -8.881784197001246407E-16, 2.361472542561082612E-16, -1.000000000000000000 ) ) ;
#885=DIRECTION ( 'NONE',  ( -1.000000000000000000, -2.276539994720197063E-15, 0.000000000000000000 ) ) ;
#894=DIRECTION ( 'NONE',  ( 1.000000000000000000, 1.707404996040165152E-15, 0.000000000000000000 ) ) ;
#914=DIRECTION ( 'NONE',  ( 1.445848444424219201E-15, -1.000000000000000000, -2.361472542561095431E-16 ) ) ;
#940=AXIS2_PLACEMENT_3D ( 'NONE', #30986, #31207, #2810 ) ;
#957=AXIS2_PLACEMENT_3D ( 'NONE', #14940, #29606, #7592 ) ;
#962=CARTESIAN_POINT ( 'NONE',  ( -0.2267371898560526788, -0.4872893062166341327, 0.09999999999999975575 ) ) ;
#982=FACE_OUTER_BOUND ( 'NONE', #34433, .T. ) ;
#991=CARTESIAN_POINT ( 'NONE',  ( -0.1552056223146404124, 0.4812861443614839807, 0.3591723288241695511 ) ) ;
#1126=( CONVERSION_BASED_UNIT ( 'INCH', #10967 ) LENGTH_UNIT ( ) NAMED_UNIT ( #23398 ) );
#1129=AXIS2_PLACEMENT_3D ( 'NONE', #18383, #36706, #24181 ) ;
#1147=B_SPLINE_CURVE_WITH_KNOTS ( 'NONE', 3,
 ( #33606, #5416, #27653, #30931, #17981, #19424, #28673, #28867 ),
 .UNSPECIFIED., .F., .F.,
 ( 4, 2, 2, 4 ),
 ( -8.478460988836644674E-17, 0.0008552058350302836837, 0.001282808752545466129, 0.001710411670060648683 ),
 .UNSPECIFIED. ) ;
#1206=EDGE_CURVE ( 'NONE', #1887, #18158, #5122, .T. ) ;
#1237=CIRCLE ( 'NONE', #21573, 0.01500000000000002894 ) ;
#1249=VERTEX_POINT ( 'NONE', #962 ) ;
#1259=EDGE_CURVE ( 'NONE', #18158, #33923, #16312, .T. ) ;
#1272=EDGE_CURVE ( 'NONE', #7197, #29556, #1237, .T. ) ;
#1285=DIRECTION ( 'NONE',  ( -1.000000000000000000, -1.450080480853946466E-15, 8.188689774234050758E-16 ) ) ;
#1297=EDGE_CURVE ( 'NONE', #19690, #11981, #3809, .T. ) ;
#1359=ORIENTED_EDGE ( 'NONE', *, *, #22868, .F. ) ;
#1365=AXIS2_PLACEMENT_3D ( 'NONE', #21193, #33953, #37234 ) ;
#1371=LINE ( 'NONE', #39392, #38362 ) ;
#1375=CARTESIAN_POINT ( 'NONE',  ( -0.1638575715552559042, 0.5090525736530187029, 0.3414257732885224161 ) ) ;
#1385=ORIENTED_EDGE ( 'NONE', *, *, #29103, .F. ) ;
#1427=VERTEX_POINT ( 'NONE', #20669 ) ;
#1468=ADVANCED_FACE ( 'NONE', ( #11188 ), #5007, .T. ) ;
#1471=EDGE_CURVE ( 'NONE', #27541, #10276, #3949, .T. ) ;
#1482=ORIENTED_EDGE ( 'NONE', *, *, #38374, .T. ) ;
#1531=ORIENTED_EDGE ( 'NONE', *, *, #28760, .T. ) ;
#1546=CIRCLE ( 'NONE', #6765, 0.06000000000000038636 ) ;
#1572=ORIENTED_EDGE ( 'NONE', *, *, #32786, .F. ) ;
#1596=ORIENTED_EDGE ( 'NONE', *, *, #30272, .F. ) ;
#1605=AXIS2_PLACEMENT_3D ( 'NONE', #26518, #23239, #32679 ) ;
#1622=ADVANCED_FACE ( 'NONE', ( #22196, #34912, #19684 ), #34711, .T. ) ;
#1630=AXIS2_PLACEMENT_3D ( 'NONE', #12113, #9417, #27354 ) ;
#1648=B_SPLINE_CURVE_WITH_KNOTS ( 'NONE', 3,
 ( #2160, #36510, #8321, #14086, #39194, #4417, #23574, #36093 ),
 .UNSPECIFIED., .F., .F.,
 ( 4, 2, 2, 4 ),
 ( 0.0005881714484888330569, 0.001255587419990853576, 0.001589295405741864486, 0.001923003391492875396 ),
 .UNSPECIFIED. ) ;
#1718=CARTESIAN_POINT ( 'NONE',  ( -0.2300000000000000655, 0.5182417262804733804, 0.3749999999999999445 ) ) ;
#1810=DIRECTION ( 'NONE',  ( 1.000000000000000000, 1.443840457432242888E-15, -8.336459783983783483E-16 ) ) ;
#1858=DIRECTION ( 'NONE',  ( -1.000000000000000000, -1.450080480853946466E-15, 8.188689774234050758E-16 ) ) ;
#1887=VERTEX_POINT ( 'NONE', #5453 ) ;
#1896=ORIENTED_EDGE ( 'NONE', *, *, #23810, .F. ) ;
#1947=DIRECTION ( 'NONE',  ( -1.000000000000000000, -1.138269997360102279E-15, 1.138269997360102279E-15 ) ) ;
#2007=AXIS2_PLACEMENT_3D ( 'NONE', #25307, #15827, #37845 ) ;
#2013=CARTESIAN_POINT ( 'NONE',  ( -0.08408070219616067820, -0.09959325338431374020, 0.3749999999999987232 ) ) ;
#2110=EDGE_CURVE ( 'NONE', #36587, #2842, #34956, .T. ) ;
#2112=ORIENTED_EDGE ( 'NONE', *, *, #38643, .F. ) ;
#2145=EDGE_CURVE ( 'NONE', #25611, #22283, #25747, .T. ) ;
#2160=CARTESIAN_POINT ( 'NONE',  ( -0.1088121136105144049, -0.4964308608213456875, 0.1000000000000000194 ) ) ;
#2163=ORIENTED_EDGE ( 'NONE', *, *, #12309, .T. ) ;
#2166=DIRECTION ( 'NONE',  ( 8.881784197001246407E-16, -2.361472542561082612E-16, 1.000000000000000000 ) ) ;
#2283=CARTESIAN_POINT ( 'NONE',  ( -0.1157351208611889781, -0.4799584063719138927, 0.1184929141221633259 ) ) ;
#2383=EDGE_CURVE ( 'NONE', #12135, #36587, #7374, .T. ) ;
#2394=EDGE_LOOP ( 'NONE', ( #26405, #27725, #14929, #2495, #20764, #36435 ) ) ;
#2461=CARTESIAN_POINT ( 'NONE',  ( -0.1157351144566549916, -0.4800210170678197441, 0.3382895569178748785 ) ) ;
#2483=CARTESIAN_POINT ( 'NONE',  ( -0.1062912471183645874, -0.4837944836747484212, 0.1097058945452955153 ) ) ;
#2495=ORIENTED_EDGE ( 'NONE', *, *, #4868, .T. ) ;
#2508=ADVANCED_FACE ( 'NONE', ( #11703 ), #14765, .T. ) ;
#2561=DIRECTION ( 'NONE',  ( 8.881784197001246407E-16, -2.361472542561082612E-16, 1.000000000000000000 ) ) ;
#2571=ORIENTED_EDGE ( 'NONE', *, *, #6884, .F. ) ;
#2573=CARTESIAN_POINT ( 'NONE',  ( -0.1212602504878801113, -0.5073146173917535418, 0.1528658435936971483 ) ) ;
#2649=CIRCLE ( 'NONE', #15109, 0.03000000000000029379 ) ;
#2674=CYLINDRICAL_SURFACE ( 'NONE', #13172, 0.03000000000000008910 ) ;
#2676=CARTESIAN_POINT ( 'NONE',  ( -0.1056392956507297559, -0.4804620820570389972, 0.09550516425354510508 ) ) ;
#2762=DIRECTION ( 'NONE',  ( 1.000000000000000000, 1.450080480853946466E-15, -8.359287477863926836E-16 ) ) ;
#2764=LINE ( 'NONE', #33611, #32435 ) ;
#2774=CARTESIAN_POINT ( 'NONE',  ( -0.1163549140004252191, -0.5320595946631425655, 0.1429098354137926519 ) ) ;
#2775=VERTEX_POINT ( 'NONE', #40023 ) ;
#2810=DIRECTION ( 'NONE',  ( 1.000000000000000000, 1.138269997360101095E-15, -8.537024980200757723E-16 ) ) ;
#2827=DIRECTION ( 'NONE',  ( -1.000000000000000000, -1.138269997360101095E-15, 1.138269997360101095E-15 ) ) ;
#2842=VERTEX_POINT ( 'NONE', #15348 ) ;
#2853=CARTESIAN_POINT ( 'NONE',  ( -0.1190701091186102401, -0.4967104654273956088, 0.3286746847624749668 ) ) ;
#2873=AXIS2_PLACEMENT_3D ( 'NONE', #11161, #4378, #16738 ) ;
#2874=VERTEX_POINT ( 'NONE', #9159 ) ;
#2885=DIRECTION ( 'NONE',  ( -0.05576617209162638977, -0.2535907321156579686, 0.9657027879401052228 ) ) ;
#2907=CIRCLE ( 'NONE', #21296, 2.001671648589477215 ) ;
#2928=AXIS2_PLACEMENT_3D ( 'NONE', #16307, #22091, #34611 ) ;
#2952=CARTESIAN_POINT ( 'NONE',  ( -0.1696269498702784040, 0.4941072959623545868, 0.1354043093116672480 ) ) ;
#2959=CARTESIAN_POINT ( 'NONE',  ( -0.1533385355407300699, 0.4750492940987078305, 0.3599999999999999867 ) ) ;
#2961=DIRECTION ( 'NONE',  ( 0.000000000000000000, 0.000000000000000000, 1.000000000000000000 ) ) ;
#2999=ORIENTED_EDGE ( 'NONE', *, *, #7874, .T. ) ;
#3039=EDGE_LOOP ( 'NONE', ( #23609, #10377, #8626, #39961, #9208, #10298, #2163, #3851 ) ) ;
#3096=CARTESIAN_POINT ( 'NONE',  ( -0.1450923023275085544, -0.5230583524814751417, 0.1380392329925464179 ) ) ;
#3137=ORIENTED_EDGE ( 'NONE', *, *, #7908, .F. ) ;
#3156=LENGTH_MEASURE_WITH_UNIT ( LENGTH_MEASURE( 0.02539999999999999897 ), #25581 );
#3185=DIRECTION ( 'NONE',  ( 8.881784197001246407E-16, -2.361472542561082612E-16, 1.000000000000000000 ) ) ;
#3223=EDGE_CURVE ( 'NONE', #17694, #31075, #21360, .T. ) ;
#3252=CARTESIAN_POINT ( 'NONE',  ( -0.1133687188271738921, -0.5183431199920780497, 0.3403596628068928376 ) ) ;
#3331=TOROIDAL_SURFACE ( 'NONE', #7252, 0.04500000000000023426, 0.01499999999999999944 ) ;
#3334=CARTESIAN_POINT ( 'NONE',  ( -0.1595531559346308192, 0.4954596757340662960, 0.1197284696570143359 ) ) ;
#3346=CARTESIAN_POINT ( 'NONE',  ( -0.1059790098053070145, -0.4816261856389995044, 0.09813923389061121605 ) ) ;
#3432=FACE_OUTER_BOUND ( 'NONE', #37588, .T. ) ;
#3447=CARTESIAN_POINT ( 'NONE',  ( -0.1210148435730035998, -0.5061394519556905447, 0.1438724812234790928 ) ) ;
#3562=CARTESIAN_POINT ( 'NONE',  ( -0.1088121136105144049, -0.4964308608213456875, 0.1000000000000000194 ) ) ;
#3651=ADVANCED_FACE ( 'NONE', ( #20221 ), #25998, .F. ) ;
#3722=DIRECTION ( 'NONE',  ( 8.881784197001245421E-16, -2.361472542561082612E-16, 1.000000000000000000 ) ) ;
#3794=VERTEX_POINT ( 'NONE', #11566 ) ;
#3809=CIRCLE ( 'NONE', #6437, 0.03000000000000029379 ) ;
#3816=FACE_BOUND ( 'NONE', #30802, .T. ) ;
#3823=CARTESIAN_POINT ( 'NONE',  ( -0.1613941814439339706, 0.5013693833954219192, 0.3301047373962494036 ) ) ;
#3840=ORIENTED_EDGE ( 'NONE', *, *, #6884, .T. ) ;
#3851=ORIENTED_EDGE ( 'NONE', *, *, #10449, .F. ) ;
#3883=EDGE_LOOP ( 'NONE', ( #34607, #18105, #4572, #21562, #35821, #1572 ) ) ;
#3949=CIRCLE ( 'NONE', #12502, 1.991674066779354213 ) ;
#3950=DIRECTION ( 'NONE',  ( -1.000000000000000000, -2.276539994720197063E-15, 0.000000000000000000 ) ) ;
#3954=( NAMED_UNIT ( * ) SI_UNIT ( $, .STERADIAN. ) SOLID_ANGLE_UNIT ( ) );
#3974=ORIENTED_EDGE ( 'NONE', *, *, #3223, .T. ) ;
#4012=DIRECTION ( 'NONE',  ( 1.000000000000000000, 1.445848444424219398E-15, -8.326672684688652360E-16 ) ) ;
#4016=DIRECTION ( 'NONE',  ( 1.000000000000000000, 5.586287484112844226E-16, -8.336459783983783483E-16 ) ) ;
#4020=CARTESIAN_POINT ( 'NONE',  ( -0.1589247078933331003, 0.4934387919091514085, 0.3384493358270195262 ) ) ;
#4059=CARTESIAN_POINT ( 'NONE',  ( -0.1210148435730253463, -0.5061394519557904648, 0.3122829191279373751 ) ) ;
#4062=CIRCLE ( 'NONE', #27074, 0.9087847906030154244 ) ;
#4096=CIRCLE ( 'NONE', #25796, 0.06000000000000038636 ) ;
#4184=AXIS2_PLACEMENT_3D ( 'NONE', #6899, #34884, #25232 ) ;
#4233=CARTESIAN_POINT ( 'NONE',  ( -0.1710642718812864782, 0.4986889572247779068, 0.3032895567580807250 ) ) ;
#4327=DIRECTION ( 'NONE',  ( -8.881784197001246407E-16, 2.361472542561082612E-16, -1.000000000000000000 ) ) ;
#4355=ORIENTED_EDGE ( 'NONE', *, *, #26795, .F. ) ;
#4378=DIRECTION ( 'NONE',  ( 8.881784197001246407E-16, -2.361472542561082612E-16, 1.000000000000000000 ) ) ;
#4405=ORIENTED_EDGE ( 'NONE', *, *, #7874, .F. ) ;
#4417=CARTESIAN_POINT ( 'NONE',  ( -0.1151895542371778602, -0.5267561842548691420, 0.1296992319623858358 ) ) ;
#4419=DIRECTION ( 'NONE',  ( 8.881784197001246407E-16, -2.361472542561082612E-16, 1.000000000000000000 ) ) ;
#4433=CARTESIAN_POINT ( 'NONE',  ( -0.1656893171628753825, 0.4813634391809688551, 0.3338433979331971169 ) ) ;
#4488=DIRECTION ( 'NONE',  ( 1.000000000000000000, 1.441651681710401470E-15, -8.317221240636930495E-16 ) ) ;
#4498=CARTESIAN_POINT ( 'NONE',  ( -0.1684323895664678050, 0.5231977504175356897, 0.1528658435937002014 ) ) ;
#4518=CARTESIAN_POINT ( 'NONE',  ( -0.1455608194604309513, -0.5249067277714104529, 0.1528658435937002014 ) ) ;
#4550=DIRECTION ( 'NONE',  ( -8.881784197001245421E-16, 2.361472542561082612E-16, -1.000000000000000000 ) ) ;
#4566=DIRECTION ( 'NONE',  ( -8.881784197001245421E-16, 2.361472542561082612E-16, -1.000000000000000000 ) ) ;
#4572=ORIENTED_EDGE ( 'NONE', *, *, #37391, .T. ) ;
#4579=EDGE_CURVE ( 'NONE', #19668, #4809, #20125, .T. ) ;
#4606=DIRECTION ( 'NONE',  ( -8.881784197001246407E-16, 2.361472542561082612E-16, -1.000000000000000000 ) ) ;
#4608=AXIS2_PLACEMENT_3D ( 'NONE', #21383, #24670, #8586 ) ;
#4654=CARTESIAN_POINT ( 'NONE',  ( -0.1127677449505065793, -0.5183788106020520425, 0.3108513529155225164 ) ) ;
#4672=CARTESIAN_POINT ( 'NONE',  ( -0.1212602504878780296, -0.5073146173917506552, 0.3749999999999999445 ) ) ;
#4717=DIRECTION ( 'NONE',  ( -9.106159978880870295E-15, 1.000000000000000000, -2.845674993400271967E-15 ) ) ;
#4719=ORIENTED_EDGE ( 'NONE', *, *, #17641, .F. ) ;
#4780=DIRECTION ( 'NONE',  ( 0.2828184691483945357, -0.9591734532964090176, 3.801289047037795017E-15 ) ) ;
#4803=CARTESIAN_POINT ( 'NONE',  ( -0.2900000000000005351, 0.5182417262804733804, 0.3750000000000000555 ) ) ;
#4809=VERTEX_POINT ( 'NONE', #31146 ) ;
#4868=EDGE_CURVE ( 'NONE', #36928, #2775, #20287, .T. ) ;
#4869=CARTESIAN_POINT ( 'NONE',  ( -0.2789010053595599725, 0.4834754829570387935, 0.1000000000000000194 ) ) ;
#4879=VERTEX_POINT ( 'NONE', #12412 ) ;
#4886=DIRECTION ( 'NONE',  ( 8.881784197001246407E-16, -2.361472542561082612E-16, 1.000000000000000000 ) ) ;
#4891=VERTEX_POINT ( 'NONE', #6624 ) ;
#4893=CIRCLE ( 'NONE', #27912, 0.03000000000000029379 ) ;
#4936=AXIS2_PLACEMENT_3D ( 'NONE', #6271, #6466, #24608 ) ;
#4970=TOROIDAL_SURFACE ( 'NONE', #33886, 0.04500000000000032446, 0.01499999999999999944 ) ;
#5007=CYLINDRICAL_SURFACE ( 'NONE', #14457, 0.06000000000000038636 ) ;
#5011=VERTEX_POINT ( 'NONE', #22918 ) ;
#5122=CIRCLE ( 'NONE', #37313, 0.01499999999999999424 ) ;
#5134=ORIENTED_EDGE ( 'NONE', *, *, #20063, .F. ) ;
#5139=ADVANCED_FACE ( 'NONE', ( #19349 ), #25518, .T. ) ;
#5190=VERTEX_POINT ( 'NONE', #9461 ) ;
#5206=VERTEX_POINT ( 'NONE', #22242 ) ;
#5264=CARTESIAN_POINT ( 'NONE',  ( -0.1603938765018561030, 0.4636889572247975266, 0.3382895567582887564 ) ) ;
#5298=CARTESIAN_POINT ( 'NONE',  ( -0.1530923209794422257, 0.4738745695581272344, 0.09813923389055254076 ) ) ;
#5299=FACE_OUTER_BOUND ( 'NONE', #21620, .T. ) ;
#5312=TOROIDAL_SURFACE ( 'NONE', #19813, 0.04500000000000023426, 0.01499999999999999944 ) ;
#5318=DIRECTION ( 'NONE',  ( -0.4887635750373031107, -0.8724162812079762075, 4.177458024893467913E-17 ) ) ;
#5325=CARTESIAN_POINT ( 'NONE',  ( -0.1044436713285806784, -0.4741860147766130407, 0.09550516381870173543 ) ) ;
#5350=AXIS2_PLACEMENT_3D ( 'NONE', #13602, #16478, #38077 ) ;
#5383=EDGE_LOOP ( 'NONE', ( #14112, #30826, #2571, #17555 ) ) ;
#5416=CARTESIAN_POINT ( 'NONE',  ( -0.1151536691905414717, -0.5265970617445885349, 0.3290111518013588698 ) ) ;
#5422=DIRECTION ( 'NONE',  ( 8.881784197001245421E-16, -2.361472542561082612E-16, 1.000000000000000000 ) ) ;
#5453=CARTESIAN_POINT ( 'NONE',  ( -0.1107910466892926965, -0.04310840302198015728, 0.09999999999999895084 ) ) ;
#5478=CARTESIAN_POINT ( 'NONE',  ( -0.1443922129835731594, -0.5166151207188711680, 0.3749999999999999445 ) ) ;
#5495=ORIENTED_EDGE ( 'NONE', *, *, #2383, .T. ) ;
#5545=CARTESIAN_POINT ( 'NONE',  ( -2.070754768975508586, -0.09959325338431662678, 0.3600000000000021516 ) ) ;
#5546=CARTESIAN_POINT ( 'NONE',  ( -0.1111952754772430191, -0.5081759048641460996, 0.1244868412816072106 ) ) ;
#5549=EDGE_LOOP ( 'NONE', ( #40368, #31161, #39101, #32810, #26372 ) ) ;
#5618=ADVANCED_FACE ( 'NONE', ( #32058 ), #32902, .T. ) ;
#5619=CARTESIAN_POINT ( 'NONE',  ( -0.1631212487981108517, 0.5067506594879367388, 0.1120476149576248998 ) ) ;
#5645=AXIS2_PLACEMENT_3D ( 'NONE', #20462, #14081, #17585 ) ;
#5710=EDGE_LOOP ( 'NONE', ( #19824, #13050, #14817, #5134 ) ) ;
#5743=CARTESIAN_POINT ( 'NONE',  ( -0.2900000000000005906, 0.5182417262804733804, 0.1000000000000000749 ) ) ;
#5768=ORIENTED_EDGE ( 'NONE', *, *, #31035, .F. ) ;
#5789=DIRECTION ( 'NONE',  ( -8.881784197001246407E-16, 2.361472542561082612E-16, -1.000000000000000000 ) ) ;
#5827=ORIENTED_EDGE ( 'NONE', *, *, #21997, .F. ) ;
#5846=VERTEX_POINT ( 'NONE', #18868 ) ;
#5853=CARTESIAN_POINT ( 'NONE',  ( -0.09579104668929040722, -0.04310840302198015034, 0.09999999999999897859 ) ) ;
#5939=CIRCLE ( 'NONE', #2007, 0.01500000000000001679 ) ;
#5969=AXIS2_PLACEMENT_3D ( 'NONE', #33083, #32683, #4488 ) ;
#6045=EDGE_LOOP ( 'NONE', ( #4719, #20454, #37933, #9548 ) ) ;
#6085=CARTESIAN_POINT ( 'NONE',  ( -0.1969433606228568612, 0.5138636982738121750, 0.3749999999999991673 ) ) ;
#6127=CARTESIAN_POINT ( 'NONE',  ( -0.1129900121204308744, -0.5167580615070271888, 0.3146079272632520962 ) ) ;
#6129=CIRCLE ( 'NONE', #34386, 2.001674066779353556 ) ;
#6149=ORIENTED_EDGE ( 'NONE', *, *, #26795, .T. ) ;
#6151=EDGE_LOOP ( 'NONE', ( #27999, #15134, #14648, #22133, #3974 ) ) ;
#6228=CARTESIAN_POINT ( 'NONE',  ( -0.1631308187679522681, 0.4729065765976254165, 0.1187908002253836859 ) ) ;
#6263=AXIS2_PLACEMENT_3D ( 'NONE', #28848, #312, #38706 ) ;
#6271=CARTESIAN_POINT ( 'NONE',  ( -0.1455608194604307570, -0.5249067277714107860, 0.3032895567580802809 ) ) ;
#6275=CARTESIAN_POINT ( 'NONE',  ( -0.1969433606228592482, 0.5138636982738209458, 0.3032895567580813356 ) ) ;
#6386=PRODUCT_DEFINITION ( 'UNKNOWN', '', #24016, #39289 ) ;
#6437=AXIS2_PLACEMENT_3D ( 'NONE', #25429, #16764, #19039 ) ;
#6466=DIRECTION ( 'NONE',  ( 8.881784197001246407E-16, -2.361472542561082612E-16, 1.000000000000000000 ) ) ;
#6470=DIRECTION ( 'NONE',  ( -0.2147743920926310501, -0.9766636885342062646, -4.525659028955483907E-15 ) ) ;
#6554=FACE_OUTER_BOUND ( 'NONE', #22465, .T. ) ;
#6608=TOROIDAL_SURFACE ( 'NONE', #15174, 0.9237847906030132172, 0.01499999999999999944 ) ;
#6611=CARTESIAN_POINT ( 'NONE',  ( -0.1688425296110704910, 0.4915895952456253437, 0.1316117873487812617 ) ) ;
#6623=EDGE_CURVE ( 'NONE', #23460, #35126, #35288, .T. ) ;
#6624=CARTESIAN_POINT ( 'NONE',  ( -0.2600000000000008415, 0.5182417262804733804, 0.08500000000000006162 ) ) ;
#6680=ADVANCED_FACE ( 'NONE', ( #19579 ), #10340, .T. ) ;
#6765=AXIS2_PLACEMENT_3D ( 'NONE', #38428, #10448, #636 ) ;
#6786=DIRECTION ( 'NONE',  ( -8.881784197001246407E-16, 2.361472542561082612E-16, -1.000000000000000000 ) ) ;
#6831=CIRCLE ( 'NONE', #10787, 0.04500000000000033834 ) ;
#6875=DIRECTION ( 'NONE',  ( 0.9766636885342062646, -0.2147743920926303007, 0.000000000000000000 ) ) ;
#6884=EDGE_CURVE ( 'NONE', #19865, #40308, #21701, .T. ) ;
#6899=CARTESIAN_POINT ( 'NONE',  ( -1.019575837292305609, -0.04310840302198155199, 0.3599999999999999867 ) ) ;
#6909=CARTESIAN_POINT ( 'NONE',  ( -0.1668894944044049256, 0.4852776769345336638, 0.3312153816179680410 ) ) ;
#6953=CARTESIAN_POINT ( 'NONE',  ( -0.1126900943355827051, -0.5191528601550228217, 0.3070571034468279059 ) ) ;
#6962=LINE ( 'NONE', #10455, #27697 ) ;
#7038=CARTESIAN_POINT ( 'NONE',  ( -0.1613941803225988625, 0.5013693709968661816, 0.1260513636289518347 ) ) ;
#7100=CARTESIAN_POINT ( 'NONE',  ( -0.1542173385434630895, 0.4780076866987719719, 0.3460825593793663835 ) ) ;
#7119=ORIENTED_EDGE ( 'NONE', *, *, #34048, .T. ) ;
#7133=EDGE_CURVE ( 'NONE', #11981, #19690, #2649, .T. ) ;
#7142=EDGE_CURVE ( 'NONE', #10109, #9291, #6962, .T. ) ;
#7151=ORIENTED_EDGE ( 'NONE', *, *, #34872, .T. ) ;
#7156=CARTESIAN_POINT ( 'NONE',  ( -0.1304423469995341367, -0.5262799683630393632, 0.1000000000000000194 ) ) ;
#7158=DIRECTION ( 'NONE',  ( -8.881784197001246407E-16, 2.361472542561082612E-16, -1.000000000000000000 ) ) ;
#7168=DIRECTION ( 'NONE',  ( -1.000000000000000000, -1.138269997360101095E-15, 1.138269997360101095E-15 ) ) ;
#7197=VERTEX_POINT ( 'NONE', #28584 ) ;
#7200=DIRECTION ( 'NONE',  ( 1.445848444424219201E-15, -1.000000000000000000, -2.361472542561095431E-16 ) ) ;
#7252=AXIS2_PLACEMENT_3D ( 'NONE', #20949, #4886, #33471 ) ;
#7297=CARTESIAN_POINT ( 'NONE',  ( -0.1683849832494421772, 0.4901165368553623281, 0.3263506530379017834 ) ) ;
#7340=AXIS2_PLACEMENT_3D ( 'NONE', #33712, #14187, #14581 ) ;
#7344=CARTESIAN_POINT ( 'NONE',  ( -0.2043922129835736845, -0.5166151207188713901, 0.3749999999999999445 ) ) ;
#7374=LINE ( 'NONE', #16268, #18018 ) ;
#7396=DIRECTION ( 'NONE',  ( 1.000000000000000000, 1.443840457432242888E-15, -8.250516899612815800E-16 ) ) ;
#7406=DIRECTION ( 'NONE',  ( -1.000000000000000000, -2.276539994720197063E-15, 5.691349986800492658E-16 ) ) ;
#7433=CIRCLE ( 'NONE', #12701, 0.9087847906030154244 ) ;
#7547=CARTESIAN_POINT ( 'NONE',  ( -0.1617315581917541378, 0.4682256792068176243, 0.1178658435936995874 ) ) ;
#7592=DIRECTION ( 'NONE',  ( 1.000000000000000000, 3.035386659626936255E-15, -7.588466649067340637E-16 ) ) ;
#7631=ORIENTED_EDGE ( 'NONE', *, *, #25370, .T. ) ;
#7634=EDGE_CURVE ( 'NONE', #39928, #12063, #25676, .T. ) ;
#7683=ORIENTED_EDGE ( 'NONE', *, *, #36333, .T. ) ;
#7718=DIRECTION ( 'NONE',  ( -1.000000000000000000, -1.441634041478669458E-15, 8.359771364787550201E-16 ) ) ;
#7753=CARTESIAN_POINT ( 'NONE',  ( -0.1630577892339038493, 0.4726628520879604944, 0.1187338422647632452 ) ) ;
#7776=DIRECTION ( 'NONE',  ( 8.881784197001246407E-16, -2.361472542561082612E-16, 1.000000000000000000 ) ) ;
#7819=ORIENTED_EDGE ( 'NONE', *, *, #39675, .T. ) ;
#7841=CARTESIAN_POINT ( 'NONE',  ( -0.1142670043590670176, -0.4723146173917492918, 0.1178658435936998927 ) ) ;
#7846=CARTESIAN_POINT ( 'NONE',  ( -0.1157108546715163999, -0.4798936717283854292, 0.3382895567580818663 ) ) ;
#7859=LINE ( 'NONE', #27433, #31630 ) ;
#7874=EDGE_CURVE ( 'NONE', #21489, #5206, #5939, .T. ) ;
#7908=EDGE_CURVE ( 'NONE', #18566, #33923, #13818, .T. ) ;
#7923=ADVANCED_FACE ( 'NONE', ( #12535 ), #28945, .T. ) ;
#7942=CARTESIAN_POINT ( 'NONE',  ( -0.1667768525404941804, 0.4849111360356616052, 0.1246604372685278656 ) ) ;
#7991=ADVANCED_FACE ( 'NONE', ( #31466 ), #2674, .T. ) ;
#8014=ORIENTED_EDGE ( 'NONE', *, *, #14816, .F. ) ;
#8043=CARTESIAN_POINT ( 'NONE',  ( -0.1157923916715206808, -0.5295015842444287246, 0.3749999999999999445 ) ) ;
#8156=CARTESIAN_POINT ( 'NONE',  ( -0.1710642718812834251, 0.4986889572247755198, 0.1528658435937002014 ) ) ;
#8183=LINE ( 'NONE', #4672, #34873 ) ;
#8205=AXIS2_PLACEMENT_3D ( 'NONE', #35826, #29648, #35615 ) ;
#8206=CARTESIAN_POINT ( 'NONE',  ( -2.070754768975509474, -0.09959325338431662678, 0.3750000000000004996 ) ) ;
#8226=ORIENTED_EDGE ( 'NONE', *, *, #31394, .F. ) ;
#8249=EDGE_CURVE ( 'NONE', #30856, #19865, #29492, .T. ) ;
#8277=EDGE_CURVE ( 'NONE', #20283, #40308, #8183, .T. ) ;
#8278=AXIS2_PLACEMENT_3D ( 'NONE', #14336, #11467, #33456 ) ;
#8315=DIRECTION ( 'NONE',  ( 1.000000000000000000, 0.000000000000000000, 0.000000000000000000 ) ) ;
#8321=CARTESIAN_POINT ( 'NONE',  ( -0.1119307826792329957, -0.5115903042181111360, 0.1085569730127855792 ) ) ;
#8330=EDGE_LOOP ( 'NONE', ( #5827, #25202, #9753, #12700, #31011, #22428 ) ) ;
#8366=CARTESIAN_POINT ( 'NONE',  ( -0.1873388932668325069, 0.5325605939836577374, 0.08499999999999950651 ) ) ;
#8397=ADVANCED_FACE ( 'NONE', ( #33076 ), #6608, .T. ) ;
#8407=ADVANCED_FACE ( 'NONE', ( #11079 ), #3331, .T. ) ;
#8426=ORIENTED_EDGE ( 'NONE', *, *, #10148, .F. ) ;
#8431=CARTESIAN_POINT ( 'NONE',  ( -0.1196081096344516342, -0.4993394475604094884, 0.1302951649420520941 ) ) ;
#8471=EDGE_CURVE ( 'NONE', #35865, #25611, #27017, .T. ) ;
#8586=DIRECTION ( 'NONE',  ( -1.000000000000000000, -2.276539994720197063E-15, 0.000000000000000000 ) ) ;
#8613=AXIS2_PLACEMENT_3D ( 'NONE', #13189, #25554, #1285 ) ;
#8626=ORIENTED_EDGE ( 'NONE', *, *, #18193, .T. ) ;
#8647=DIRECTION ( 'NONE',  ( -8.881784197001245421E-16, 2.361472542561082612E-16, -1.000000000000000000 ) ) ;
#8669=AXIS2_PLACEMENT_3D ( 'NONE', #27963, #37404, #40502 ) ;
#8698=ORIENTED_EDGE ( 'NONE', *, *, #2110, .T. ) ;
#8700=CARTESIAN_POINT ( 'NONE',  ( -0.1684323895664706916, 0.5231977504175452376, 0.1471384328909199346 ) ) ;
#8742=ORIENTED_EDGE ( 'NONE', *, *, #16286, .F. ) ;
#8749=DIRECTION ( 'NONE',  ( 1.000000000000000000, 1.707404996040165152E-15, 0.000000000000000000 ) ) ;
#8795=VERTEX_POINT ( 'NONE', #23404 ) ;
#8835=CARTESIAN_POINT ( 'NONE',  ( -0.2136509456379323546, -0.4946207598421927254, 0.3599999999999999867 ) ) ;
#8844=CARTESIAN_POINT ( 'NONE',  ( -0.1190772264498491800, -0.4967457283353927111, 0.1275078045371871027 ) ) ;
#8903=CARTESIAN_POINT ( 'NONE',  ( -0.2343922129835739054, -0.5166151207188712791, 0.1000000000000000749 ) ) ;
#8918=LINE ( 'NONE', #27254, #15325 ) ;
#8920=CARTESIAN_POINT ( 'NONE',  ( 0.000000000000000000, 0.000000000000000000, 0.000000000000000000 ) ) ;
#8944=CARTESIAN_POINT ( 'NONE',  ( -0.1211791774340324757, -0.5069275750892242582, 0.1468366819525770417 ) ) ;
#8955=CIRCLE ( 'NONE', #1129, 0.01500000000000004281 ) ;
#9041=DIRECTION ( 'NONE',  ( 1.000000000000000000, 1.138269997360101095E-15, -8.537024980200757723E-16 ) ) ;
#9092=ORIENTED_EDGE ( 'NONE', *, *, #17973, .T. ) ;
#9126=CARTESIAN_POINT ( 'NONE',  ( -0.1212185687160894504, -0.5071153897904228103, 0.3078438592385183692 ) ) ;
#9143=ADVANCED_FACE ( 'NONE', ( #16157 ), #5312, .T. ) ;
#9159=CARTESIAN_POINT ( 'NONE',  ( -0.1684323895664525950, 0.5231977504174881721, 0.3032895567580808360 ) ) ;
#9177=FACE_OUTER_BOUND ( 'NONE', #18198, .T. ) ;
#9200=CYLINDRICAL_SURFACE ( 'NONE', #4608, 0.03000000000000029379 ) ;
#9208=ORIENTED_EDGE ( 'NONE', *, *, #8249, .T. ) ;
#9212=EDGE_CURVE ( 'NONE', #18566, #1887, #19785, .T. ) ;
#9223=DIRECTION ( 'NONE',  ( -8.881784197001246407E-16, 2.361472542561082612E-16, -1.000000000000000000 ) ) ;
#9235=DIRECTION ( 'NONE',  ( -8.881784197001246407E-16, 2.361472542561082612E-16, -1.000000000000000000 ) ) ;
#9252=ORIENTED_EDGE ( 'NONE', *, *, #7142, .F. ) ;
#9291=VERTEX_POINT ( 'NONE', #8903 ) ;
#9305=DIRECTION ( 'NONE',  ( 1.000000000000000000, 1.707404996040164166E-15, 0.000000000000000000 ) ) ;
#9306=CARTESIAN_POINT ( 'NONE',  ( -0.1524980003305985987, 0.4722686132664217773, 0.1089215716292313701 ) ) ;
#9312=CARTESIAN_POINT ( 'NONE',  ( -0.1653405084325597907, 0.5136906775330227770, 0.3358539725464960157 ) ) ;
#9374=CARTESIAN_POINT ( 'NONE',  ( -1.019575837292305609, -0.04310840302198155199, 0.3599999999999999867 ) ) ;
#9379=CARTESIAN_POINT ( 'NONE',  ( -0.1710642718812834251, 0.4986889572247755198, 0.1528658435937002014 ) ) ;
#9382=ORIENTED_EDGE ( 'NONE', *, *, #2145, .T. ) ;
#9395=DIRECTION ( 'NONE',  ( 1.000000000000000000, 1.450080480853946466E-15, -8.881784197001242463E-16 ) ) ;
#9402=CARTESIAN_POINT ( 'NONE',  ( -0.2136509456379324934, -0.4946207598421927254, 0.3749999999999996669 ) ) ;
#9409=VERTEX_POINT ( 'NONE', #28049 ) ;
#9417=DIRECTION ( 'NONE',  ( 8.881784197001246407E-16, -2.361472542561082612E-16, 1.000000000000000000 ) ) ;
#9439=AXIS2_PLACEMENT_3D ( 'NONE', #773, #4419, #12886 ) ;
#9442=TOROIDAL_SURFACE ( 'NONE', #2873, 1.986674066779348768, 0.01499999999999999944 ) ;
#9444=AXIS2_PLACEMENT_3D ( 'NONE', #25310, #7158, #10283 ) ;
#9461=CARTESIAN_POINT ( 'NONE',  ( -0.1304423469995342755, -0.5262799683630393632, 0.08499999999999922895 ) ) ;
#9548=ORIENTED_EDGE ( 'NONE', *, *, #36368, .F. ) ;
#9581=CARTESIAN_POINT ( 'NONE',  ( -0.2300000000000004818, 0.5182417262804733804, 0.3599999999999999867 ) ) ;
#9611=DIRECTION ( 'NONE',  ( 8.881784197001246407E-16, -2.361472542561082612E-16, 1.000000000000000000 ) ) ;
#9635=CARTESIAN_POINT ( 'NONE',  ( -0.1127323924368537483, -0.5155369761421360053, 0.3191796960528350824 ) ) ;
#9669=ORIENTED_EDGE ( 'NONE', *, *, #25370, .F. ) ;
#9724=CARTESIAN_POINT ( 'NONE',  ( -0.1603938765018643187, 0.4636889572248043545, 0.1178658435936973670 ) ) ;
#9753=ORIENTED_EDGE ( 'NONE', *, *, #29028, .T. ) ;
#9821=ORIENTED_EDGE ( 'NONE', *, *, #35879, .T. ) ;
#9837=CARTESIAN_POINT ( 'NONE',  ( -0.1731185243557762099, 0.5373335498847187086, 0.1000000000000000194 ) ) ;
#9838=CARTESIAN_POINT ( 'NONE',  ( -0.2300000000000004818, 0.5182417262804733804, 0.3599999999999999867 ) ) ;
#9901=CARTESIAN_POINT ( 'NONE',  ( -0.1743922129835737966, -0.5166151207188712791, 0.08499999999999977018 ) ) ;
#9918=CARTESIAN_POINT ( 'NONE',  ( -0.1659602879904968076, 0.5155992160893295706, 0.1238948718127820675 ) ) ;
#9936=DIRECTION ( 'NONE',  ( -8.881784197001246407E-16, 2.361472542561082612E-16, -1.000000000000000000 ) ) ;
#10003=CARTESIAN_POINT ( 'NONE',  ( -0.1699622337672979377, 0.4951791062278196320, 0.3187362200132128343 ) ) ;
#10004=AXIS2_PLACEMENT_3D ( 'NONE', #25993, #39131, #39322 ) ;
#10063=CIRCLE ( 'NONE', #33049, 0.03000000000000003011 ) ;
#10109=VERTEX_POINT ( 'NONE', #12263 ) ;
#10148=EDGE_CURVE ( 'NONE', #1887, #1249, #4062, .T. ) ;
#10195=CIRCLE ( 'NONE', #40399, 2.001558204291732146 ) ;
#10202=ADVANCED_FACE ( 'NONE', ( #38299 ), #643, .T. ) ;
#10210=CARTESIAN_POINT ( 'NONE',  ( -0.1107910466892924328, -0.04310840302198022667, 0.3599999999999991540 ) ) ;
#10219=CARTESIAN_POINT ( 'NONE',  ( -0.1508021419689005160, 0.4665171419162804645, 0.3606502365330792603 ) ) ;
#10225=DIRECTION ( 'NONE',  ( 1.000000000000000000, 5.544814160424620659E-16, -8.132394101956109642E-16 ) ) ;
#10256=ADVANCED_FACE ( 'NONE', ( #29048 ), #23101, .T. ) ;
#10276=VERTEX_POINT ( 'NONE', #23701 ) ;
#10283=DIRECTION ( 'NONE',  ( -1.000000000000000000, -1.446659165673941893E-15, 8.266623803851096388E-16 ) ) ;
#10298=ORIENTED_EDGE ( 'NONE', *, *, #28045, .T. ) ;
#10340=TOROIDAL_SURFACE ( 'NONE', #33313, 0.9237847906030132172, 0.01499999999999999944 ) ;
#10377=ORIENTED_EDGE ( 'NONE', *, *, #7142, .T. ) ;
#10448=DIRECTION ( 'NONE',  ( 8.881784197001246407E-16, -2.361472542561082612E-16, 1.000000000000000000 ) ) ;
#10449=EDGE_CURVE ( 'NONE', #7197, #24171, #36832, .T. ) ;
#10455=CARTESIAN_POINT ( 'NONE',  ( -0.2343922129835737667, -0.5166151207188713901, 0.3750000000000000555 ) ) ;
#10462=DIRECTION ( 'NONE',  ( -0.2147743920926263317, -0.9766636885342071528, 2.066666135092459448E-16 ) ) ;
#10487=CARTESIAN_POINT ( 'NONE',  ( -0.1743922129835737966, -0.5166151207188712791, 0.08499999999999977018 ) ) ;
#10573=CARTESIAN_POINT ( 'NONE',  ( -0.1743922129835733803, -0.5166151207188712791, 0.3749999999999999445 ) ) ;
#10601=DIRECTION ( 'NONE',  ( 1.000000000000000000, 2.276539994720212446E-15, -1.138269997360106223E-15 ) ) ;
#10637=CARTESIAN_POINT ( 'NONE',  ( -0.1603938765018536328, 0.4636889572247743230, 0.1178658435936996290 ) ) ;
#10664=CARTESIAN_POINT ( 'NONE',  ( -0.1163200376094534610, -0.5319009979872302285, 0.1426078552794932397 ) ) ;
#10712=ORIENTED_EDGE ( 'NONE', *, *, #37391, .F. ) ;
#10713=CIRCLE ( 'NONE', #33703, 1.986674066779353875 ) ;
#10775=ORIENTED_EDGE ( 'NONE', *, *, #3223, .F. ) ;
#10787=AXIS2_PLACEMENT_3D ( 'NONE', #12264, #34464, #37344 ) ;
#10808=CARTESIAN_POINT ( 'NONE',  ( -2.070754768975509474, -0.09959325338431662678, 0.3606502365330794824 ) ) ;
#10829=CARTESIAN_POINT ( 'NONE',  ( -2.070754768975509474, -0.09959325338431662678, 0.3750000000000004996 ) ) ;
#10967=LENGTH_MEASURE_WITH_UNIT ( LENGTH_MEASURE( 0.02539999999999999897 ), #38919 );
#10970=CARTESIAN_POINT ( 'NONE',  ( -0.1142670043590668788, -0.4723146173917492918, 0.3382895567580816443 ) ) ;
#10988=EDGE_CURVE ( 'NONE', #36587, #19668, #22799, .T. ) ;
#10991=VERTEX_POINT ( 'NONE', #8366 ) ;
#11079=FACE_OUTER_BOUND ( 'NONE', #18899, .T. ) ;
#11161=CARTESIAN_POINT ( 'NONE',  ( -2.070754768975509919, -0.09959325338431655739, 0.1000000000000005745 ) ) ;
#11177=DIRECTION ( 'NONE',  ( 0.9591734532964090176, 0.2828184691483947022, -5.691349986800532102E-16 ) ) ;
#11188=FACE_OUTER_BOUND ( 'NONE', #3039, .T. ) ;
#11192=CARTESIAN_POINT ( 'NONE',  ( -0.1643313925802001585, 0.5105373599712219601, 0.1162626052509345420 ) ) ;
#11238=ORIENTED_EDGE ( 'NONE', *, *, #1297, .T. ) ;
#11293=LINE ( 'NONE', #14371, #30351 ) ;
#11312=CARTESIAN_POINT ( 'NONE',  ( -0.2267371898560522903, -0.4872893062166341327, 0.3599999999999997091 ) ) ;
#11334=CIRCLE ( 'NONE', #19879, 0.03000000000000001277 ) ;
#11391=DIRECTION ( 'NONE',  ( 8.881784197001246407E-16, -2.361472542561082612E-16, 1.000000000000000000 ) ) ;
#11395=CARTESIAN_POINT ( 'NONE',  ( -0.1574377185082707353, 0.4885537809602767401, 0.1000000000000000194 ) ) ;
#11399=( GEOMETRIC_REPRESENTATION_CONTEXT ( 3 ) GLOBAL_UNCERTAINTY_ASSIGNED_CONTEXT ( ( #15737 ) ) GLOBAL_UNIT_ASSIGNED_CONTEXT ( ( #1126, #26195, #23112 ) ) REPRESENTATION_CONTEXT ( 'NONE', 'WORKASPACE' ) );
#11425=VERTEX_POINT ( 'NONE', #5743 ) ;
#11467=DIRECTION ( 'NONE',  ( 8.881784197001246407E-16, -2.361472542561082612E-16, 1.000000000000000000 ) ) ;
#11494=EDGE_CURVE ( 'NONE', #11425, #18566, #38957, .T. ) ;
#11511=FACE_OUTER_BOUND ( 'NONE', #6151, .T. ) ;
#11530=ORIENTED_EDGE ( 'NONE', *, *, #27146, .T. ) ;
#11537=CARTESIAN_POINT ( 'NONE',  ( -0.1178427669581121329, -0.4906303760369132294, 0.1227918960327501474 ) ) ;
#11566=CARTESIAN_POINT ( 'NONE',  ( -0.1061036098701638175, -0.4827967145417200179, 0.3599999999999999867 ) ) ;
#11632=DIRECTION ( 'NONE',  ( 1.000000000000000000, 1.450082232674701412E-15, -8.188699666868902382E-16 ) ) ;
#11636=FACE_OUTER_BOUND ( 'NONE', #5383, .T. ) ;
#11661=CARTESIAN_POINT ( 'NONE',  ( -0.1531325081225952400, 0.4743613400439437022, 0.3600421117866470233 ) ) ;
#11673=DIRECTION ( 'NONE',  ( 8.881784197001246407E-16, -2.361472542561082612E-16, 1.000000000000000000 ) ) ;
#11703=FACE_OUTER_BOUND ( 'NONE', #6045, .T. ) ;
#11709=EDGE_CURVE ( 'NONE', #1249, #9291, #1546, .T. ) ;
#11731=CARTESIAN_POINT ( 'NONE',  ( -0.1129900121204075181, -0.5167580615069143901, 0.1415474730881016441 ) ) ;
#11736=DIRECTION ( 'NONE',  ( 0.000000000000000000, 0.9672079024885570364, 0.2539859708009205019 ) ) ;
#11813=CARTESIAN_POINT ( 'NONE',  ( -0.1210148435730249716, -0.5061394519557976812, 0.3122829191278992389 ) ) ;
#11850=CARTESIAN_POINT ( 'NONE',  ( -0.1508044614562676355, 0.4665164580004940720, 0.3602693336111439382 ) ) ;
#11864=CARTESIAN_POINT ( 'NONE',  ( -0.1167294259372888832, -0.5331983348239500708, 0.1528658435937002014 ) ) ;
#11918=DIRECTION ( 'NONE',  ( 0.8724162812079769846, -0.4887635750373016119, 0.000000000000000000 ) ) ;
#11981=VERTEX_POINT ( 'NONE', #5478 ) ;
#11990=ADVANCED_FACE ( 'NONE', ( #18440 ), #12710, .T. ) ;
#12001=ORIENTED_EDGE ( 'NONE', *, *, #23266, .T. ) ;
#12003=CARTESIAN_POINT ( 'NONE',  ( -0.1670982076487675938, 0.5191099701766059837, 0.1307156235296929869 ) ) ;
#12034=ORIENTED_EDGE ( 'NONE', *, *, #36368, .T. ) ;
#12035=CARTESIAN_POINT ( 'NONE',  ( -0.1127636766158878062, -0.5184084763139832353, 0.1453728055589162682 ) ) ;
#12063=VERTEX_POINT ( 'NONE', #10210 ) ;
#12066=CIRCLE ( 'NONE', #34404, 0.01500000000000004281 ) ;
#12090=CIRCLE ( 'NONE', #23938, 0.01500000000000003067 ) ;
#12113=CARTESIAN_POINT ( 'NONE',  ( -2.070754768975509030, -0.09959325338431655739, 0.09550516381870291505 ) ) ;
#12135=VERTEX_POINT ( 'NONE', #9379 ) ;
#12139=DIRECTION ( 'NONE',  ( -1.000000000000000000, -2.276539994720212446E-15, 0.000000000000000000 ) ) ;
#12141=CARTESIAN_POINT ( 'NONE',  ( -0.1133606652272212828, -0.5183057948313447572, 0.1157398326556578066 ) ) ;
#12172=CARTESIAN_POINT ( 'NONE',  ( -0.1205998369024076505, -0.5041491367644056476, 0.3197686713205462050 ) ) ;
#12180=EDGE_CURVE ( 'NONE', #35064, #12063, #17957, .T. ) ;
#12222=CIRCLE ( 'NONE', #8278, 0.04500000000000044242 ) ;
#12231=ADVANCED_FACE ( 'NONE', ( #982, #3816, #28911 ), #13283, .F. ) ;
#12232=CARTESIAN_POINT ( 'NONE',  ( -0.1163196563843193754, -0.5318992644065130282, 0.3135508459095576184 ) ) ;
#12263=CARTESIAN_POINT ( 'NONE',  ( -0.2343922129835739054, -0.5166151207188712791, 0.3599999999999997646 ) ) ;
#12264=CARTESIAN_POINT ( 'NONE',  ( -0.1743922129835733803, -0.5166151207188712791, 0.3749999999999999445 ) ) ;
#12296=EDGE_CURVE ( 'NONE', #35002, #4809, #27199, .T. ) ;
#12309=EDGE_CURVE ( 'NONE', #4879, #24171, #35555, .T. ) ;
#12329=EDGE_CURVE ( 'NONE', #39928, #25455, #21950, .T. ) ;
#12395=EDGE_CURVE ( 'NONE', #5011, #2842, #2764, .T. ) ;
#12403=CARTESIAN_POINT ( 'NONE',  ( -0.1552002433785900914, 0.4812687096812806598, 0.09697487758648998257 ) ) ;
#12412=CARTESIAN_POINT ( 'NONE',  ( -0.1167294259372886750, -0.5331983348239501819, 0.3032895567580813356 ) ) ;
#12438=ORIENTED_EDGE ( 'NONE', *, *, #7133, .T. ) ;
#12457=CARTESIAN_POINT ( 'NONE',  ( -0.1212602504878780296, -0.5073146173917506552, 0.1528658435936999238 ) ) ;
#12477=( BOUNDED_SURFACE ( )  B_SPLINE_SURFACE ( 3, 2, ( 
 ( #24879, #14997, #25066 ),
 ( #37401, #24463, #2461 ),
 ( #31033, #30636, #220 ),
 ( #27746, #18478, #2853 ),
 ( #3252, #21590, #12714 ),
 ( #37819, #21395, #27550 ),
 ( #36996, #9635, #40073 ),
 ( #37599, #6127, #15402 ) ),
 .UNSPECIFIED., .F., .F., .T. ) 
 B_SPLINE_SURFACE_WITH_KNOTS ( ( 4, 2, 2, 4 ),
 ( 3, 3 ),
 ( 0.001363486440777415343, 0.002314916752335400337, 0.002790631908114392726, 0.003266347063893385548 ),
 ( 0.000000000000000000, 1.000000000000000000 ),
 .UNSPECIFIED. ) 
 GEOMETRIC_REPRESENTATION_ITEM ( )  RATIONAL_B_SPLINE_SURFACE ( (
 ( 1.000000000000000000, 0.9128709291753024369, 1.000000000000000000),
 ( 1.000000000000000000, 0.9128773865076781346, 1.000000000000000000),
 ( 1.000000000000000000, 0.9126892044518930547, 1.000000000000000000),
 ( 1.000000000000000000, 0.9123262075132244631, 1.000000000000000000),
 ( 1.000000000000000000, 0.9121926916490802340, 1.000000000000000000),
 ( 1.000000000000000000, 0.9119580040442082369, 1.000000000000000000),
 ( 1.000000000000000000, 0.9118544196726630080, 1.000000000000000000),
 ( 1.000000000000000000, 0.9117915798252037574, 1.000000000000000000) ) ) 
 REPRESENTATION_ITEM ( '' )  SURFACE ( )  );
#12497=ADVANCED_FACE ( 'NONE', ( #20236 ), #9442, .T. ) ;
#12502=AXIS2_PLACEMENT_3D ( 'NONE', #39557, #11391, #23963 ) ;
#12535=FACE_OUTER_BOUND ( 'NONE', #3883, .T. ) ;
#12601=CARTESIAN_POINT ( 'NONE',  ( -0.1612862774928120191, 0.5009394326984835111, 0.1071084547149960403 ) ) ;
#12618=ORIENTED_EDGE ( 'NONE', *, *, #1471, .T. ) ;
#12700=ORIENTED_EDGE ( 'NONE', *, *, #13484, .F. ) ;
#12701=AXIS2_PLACEMENT_3D ( 'NONE', #9374, #21954, #34481 ) ;
#12710=TOROIDAL_SURFACE ( 'NONE', #34379, 1.986674066779348768, 0.01499999999999999944 ) ;
#12714=CARTESIAN_POINT ( 'NONE',  ( -0.1196127869351430451, -0.4993621520964603988, 0.3258261256381426718 ) ) ;
#12747=CYLINDRICAL_SURFACE ( 'NONE', #9444, 0.9087847906030156464 ) ;
#12783=AXIS2_PLACEMENT_3D ( 'NONE', #8206, #23866, #1858 ) ;
#12820=CARTESIAN_POINT ( 'NONE',  ( -0.1707856549140137903, 0.4978063840003604246, 0.1437995925080443882 ) ) ;
#12886=DIRECTION ( 'NONE',  ( -1.000000000000000000, -1.448788479720435680E-15, 8.315531510821436104E-16 ) ) ;
#12940=CARTESIAN_POINT ( 'NONE',  ( -0.2300000000000005651, 0.5182417262804733804, 0.08500000000000004774 ) ) ;
#13022=CARTESIAN_POINT ( 'NONE',  ( -0.1673869564144415956, 0.4868872877193617943, 0.1265580611896311158 ) ) ;
#13050=ORIENTED_EDGE ( 'NONE', *, *, #31276, .T. ) ;
#13141=EDGE_CURVE ( 'NONE', #30856, #33568, #1371, .T. ) ;
#13172=AXIS2_PLACEMENT_3D ( 'NONE', #40309, #9235, #12139 ) ;
#13189=CARTESIAN_POINT ( 'NONE',  ( -2.070754768975509474, -0.09959325338431662678, 0.3750000000000004996 ) ) ;
#13207=ORIENTED_EDGE ( 'NONE', *, *, #28629, .T. ) ;
#13242=EDGE_CURVE ( 'NONE', #31075, #35002, #2907, .T. ) ;
#13283=PLANE ( 'NONE',  #27840 ) ;
#13358=ORIENTED_EDGE ( 'NONE', *, *, #37133, .T. ) ;
#13364=CARTESIAN_POINT ( 'NONE',  ( -0.1969433606228599420, 0.5138636982738206127, 0.1528658435937004789 ) ) ;
#13384=AXIS2_PLACEMENT_3D ( 'NONE', #37314, #21295, #21509 ) ;
#13408=AXIS2_PLACEMENT_3D ( 'NONE', #10829, #27281, #17791 ) ;
#13484=EDGE_CURVE ( 'NONE', #25919, #34346, #14742, .T. ) ;
#13507=FACE_OUTER_BOUND ( 'NONE', #29402, .T. ) ;
#13602=CARTESIAN_POINT ( 'NONE',  ( -2.070754768975508586, -0.09959325338431662678, 0.3600000000000021516 ) ) ;
#13684=FACE_OUTER_BOUND ( 'NONE', #5710, .T. ) ;
#13692=CARTESIAN_POINT ( 'NONE',  ( -0.1642263573063267590, 0.5103503758723633155, 0.3090632479873802740 ) ) ;
#13727=CARTESIAN_POINT ( 'NONE',  ( -0.1211759891752648838, -0.5069122841110333955, 0.3093762286737390954 ) ) ;
#13769=DIRECTION ( 'NONE',  ( -8.881784197001246407E-16, 2.361472542561082612E-16, -1.000000000000000000 ) ) ;
#13818=CIRCLE ( 'NONE', #1365, 0.01500000000000003067 ) ;
#13877=DIRECTION ( 'NONE',  ( -8.881784197001245421E-16, 2.361472542561082612E-16, -1.000000000000000000 ) ) ;
#13882=CARTESIAN_POINT ( 'NONE',  ( -0.1631341089705740377, 0.4729174206798267277, 0.3373594846482269038 ) ) ;
#13893=ORIENTED_EDGE ( 'NONE', *, *, #23589, .F. ) ;
#13903=CIRCLE ( 'NONE', #25083, 1.986674066779353875 ) ;
#13914=AXIS2_PLACEMENT_3D ( 'NONE', #6275, #16357, #37751 ) ;
#13931=VECTOR ( 'NONE', #8647, 39.37007874015748143 ) ;
#13946=CARTESIAN_POINT ( 'NONE',  ( -1.019575837292306053, -0.04310840302198148261, 0.09999999999999975575 ) ) ;
#13994=ORIENTED_EDGE ( 'NONE', *, *, #23531, .T. ) ;
#14026=CARTESIAN_POINT ( 'NONE',  ( -0.1212602504878780296, -0.5073146173917505442, 0.1497995784944539388 ) ) ;
#14051=ADVANCED_FACE ( 'NONE', ( #9177 ), #34277, .T. ) ;
#14081=DIRECTION ( 'NONE',  ( 0.2828184691484104119, -0.9591734532964044657, 6.098997937655262350E-13 ) ) ;
#14086=CARTESIAN_POINT ( 'NONE',  ( -0.1137534828624041094, -0.5201328034396337507, 0.1183403147931640642 ) ) ;
#14112=ORIENTED_EDGE ( 'NONE', *, *, #16286, .T. ) ;
#14152=ORIENTED_EDGE ( 'NONE', *, *, #9212, .F. ) ;
#14165=ORIENTED_EDGE ( 'NONE', *, *, #7634, .T. ) ;
#14187=DIRECTION ( 'NONE',  ( -8.881784197001246407E-16, 2.361472542561082612E-16, -1.000000000000000000 ) ) ;
#14311=ADVANCED_FACE ( 'NONE', ( #13684 ), #26249, .F. ) ;
#14336=CARTESIAN_POINT ( 'NONE',  ( -0.2300000000000000655, 0.5182417262804733804, 0.3749999999999999445 ) ) ;
#14365=CARTESIAN_POINT ( 'NONE',  ( -1.019575837292306053, -0.04310840302198148261, 0.09999999999999975575 ) ) ;
#14371=CARTESIAN_POINT ( 'NONE',  ( -0.1684323895664678050, 0.5231977504175353566, 0.3749999999999996669 ) ) ;
#14397=B_SPLINE_CURVE_WITH_KNOTS ( 'NONE', 3,
 ( #36889, #8700, #21276, #12003, #33813, #11192, #5619, #17579, #18175, #11395 ),
 .UNSPECIFIED., .F., .F.,
 ( 4, 2, 2, 2, 4 ),
 ( 7.806255641894676664E-18, 0.0004362256165457106902, 0.0008724512330914135742, 0.001308676849637116458, 0.001744902466182819342 ),
 .UNSPECIFIED. ) ;
#14401=EDGE_CURVE ( 'NONE', #25464, #17394, #10195, .T. ) ;
#14457=AXIS2_PLACEMENT_3D ( 'NONE', #10573, #30116, #1947 ) ;
#14477=DIRECTION ( 'NONE',  ( -1.000000000000000000, -1.450080480853946466E-15, 8.881784197001242463E-16 ) ) ;
#14499=EDGE_CURVE ( 'NONE', #16008, #20283, #614, .T. ) ;
#14534=CARTESIAN_POINT ( 'NONE',  ( -0.1710642718812832863, 0.4986889572247755198, 0.3032895567580813356 ) ) ;
#14574=CARTESIAN_POINT ( 'NONE',  ( -0.1509132741912892484, 0.4664843738648666305, 0.09813923389061192382 ) ) ;
#14580=CIRCLE ( 'NONE', #7340, 2.001558204291732146 ) ;
#14581=DIRECTION ( 'NONE',  ( -1.000000000000000000, -1.441634041478669458E-15, 8.359771364787550201E-16 ) ) ;
#14648=ORIENTED_EDGE ( 'NONE', *, *, #28629, .F. ) ;
#14664=VECTOR ( 'NONE', #4566, 39.37007874015748143 ) ;
#14675=CARTESIAN_POINT ( 'NONE',  ( -0.1533385355407300699, 0.4750492940987078305, 0.3599999999999999867 ) ) ;
#14711=CIRCLE ( 'NONE', #957, 0.04500000000000033834 ) ;
#14726=ADVANCED_BREP_SHAPE_REPRESENTATION ( '', ( #19057, #27819 ), #32382 ) ;
#14734=AXIS2_PLACEMENT_3D ( 'NONE', #34088, #18452, #2827 ) ;
#14742=CIRCLE ( 'NONE', #37722, 2.001674066779353556 ) ;
#14765=TOROIDAL_SURFACE ( 'NONE', #1630, 1.971674066779348866, 0.02999999999999999889 ) ;
#14816=EDGE_CURVE ( 'NONE', #35064, #1249, #17132, .T. ) ;
#14817=ORIENTED_EDGE ( 'NONE', *, *, #28069, .T. ) ;
#14822=CARTESIAN_POINT ( 'NONE',  ( -0.1210148435730082073, -0.5061394519557015359, 0.1438724812235057382 ) ) ;
#14854=CLOSED_SHELL ( 'NONE', ( #187, #2508, #11990, #8397, #31606, #26616, #14311, #30700, #1468, #29761, #10256, #36791, #5139, #20446, #30580, #23117, #1622, #12231, #3651, #21797, #27456, #129, #7923, #8407, #66, #6680, #12497, #9143, #30014, #10202, #29767, #14051, #32416, #15436, #15556, #38884, #7991, #36880, #5618 ) ) ;
#14929=ORIENTED_EDGE ( 'NONE', *, *, #17641, .T. ) ;
#14940=CARTESIAN_POINT ( 'NONE',  ( -0.1743922129835737966, -0.5166151207188712791, 0.08499999999999977018 ) ) ;
#14960=ORIENTED_EDGE ( 'NONE', *, *, #35682, .T. ) ;
#14971=CARTESIAN_POINT ( 'NONE',  ( -0.2300000000000004818, 0.5182417262804733804, 0.3599999999999999867 ) ) ;
#14997=CARTESIAN_POINT ( 'NONE',  ( -0.1044436713285788743, -0.4741860147766047695, 0.3472338286680826669 ) ) ;
#15016=ORIENTED_EDGE ( 'NONE', *, *, #12180, .F. ) ;
#15037=EDGE_LOOP ( 'NONE', ( #3840, #37333, #8226, #37513 ) ) ;
#15084=ORIENTED_EDGE ( 'NONE', *, *, #8277, .T. ) ;
#15109=AXIS2_PLACEMENT_3D ( 'NONE', #25499, #19330, #25300 ) ;
#15134=ORIENTED_EDGE ( 'NONE', *, *, #39124, .F. ) ;
#15159=CARTESIAN_POINT ( 'NONE',  ( -2.070754768975509030, -0.09959325338431662678, 0.3382895567580819218 ) ) ;
#15174=AXIS2_PLACEMENT_3D ( 'NONE', #13946, #7776, #20344 ) ;
#15190=CARTESIAN_POINT ( 'NONE',  ( -0.1045574869087419617, -0.4741643323009803734, 0.09813923389047396473 ) ) ;
#15208=CIRCLE ( 'NONE', #5350, 2.001674066779353556 ) ;
#15216=CARTESIAN_POINT ( 'NONE',  ( -0.1150001097501708036, -0.4761628310996438018, 0.1178658437130112729 ) ) ;
#15299=EDGE_CURVE ( 'NONE', #19668, #17694, #16505, .T. ) ;
#15312=CARTESIAN_POINT ( 'NONE',  ( -0.1167294259372886750, -0.5331983348239499598, 0.3084771640796422632 ) ) ;
#15325=VECTOR ( 'NONE', #21496, 39.37007874015748143 ) ;
#15348=CARTESIAN_POINT ( 'NONE',  ( -0.1669433606228592770, 0.5138636982738122860, 0.3032895567580813356 ) ) ;
#15376=FACE_OUTER_BOUND ( 'NONE', #24556, .T. ) ;
#15402=CARTESIAN_POINT ( 'NONE',  ( -0.1210148435730249716, -0.5061394519557904648, 0.3122829191279362093 ) ) ;
#15435=ORIENTED_EDGE ( 'NONE', *, *, #31276, .F. ) ;
#15436=ADVANCED_FACE ( 'NONE', ( #13507 ), #39511, .T. ) ;
#15448=AXIS2_PLACEMENT_3D ( 'NONE', #1718, #23107, #3950 ) ;
#15486=ORIENTED_EDGE ( 'NONE', *, *, #12296, .F. ) ;
#15504=CARTESIAN_POINT ( 'NONE',  ( -0.1665325656947821142, 0.5173663872579682410, 0.1272034666820740234 ) ) ;
#15529=EDGE_LOOP ( 'NONE', ( #32931, #30677, #12618, #1531, #13358, #5495, #37322, #34034, #7119, #38390, #15084 ) ) ;
#15556=ADVANCED_FACE ( 'NONE', ( #11636 ), #17424, .T. ) ;
#15690=CARTESIAN_POINT ( 'NONE',  ( -0.1656815030311168946, 0.4813244629265746033, 0.1225468705240551348 ) ) ;
#15698=( NAMED_UNIT ( * ) PLANE_ANGLE_UNIT ( ) SI_UNIT ( $, .RADIAN. ) );
#15707=ORIENTED_EDGE ( 'NONE', *, *, #28760, .F. ) ;
#15737=UNCERTAINTY_MEASURE_WITH_UNIT (LENGTH_MEASURE( 1.000000000000000082E-05 ), #1126, 'distance_accuracy_value', 'NONE');
#15746=CARTESIAN_POINT ( 'NONE',  ( -0.1515422989582873303, 0.4690188198402805986, 0.3602693336111434386 ) ) ;
#15827=DIRECTION ( 'NONE',  ( 0.5794373887239167020, -0.8150167559926659866, -6.834394190886211068E-17 ) ) ;
#15897=CARTESIAN_POINT ( 'NONE',  ( -0.1668451997768058692, 0.4851271022253518805, 0.1251051315678443909 ) ) ;
#15946=DIRECTION ( 'NONE',  ( 8.881784197001246407E-16, -2.361472542561082612E-16, 1.000000000000000000 ) ) ;
#16008=VERTEX_POINT ( 'NONE', #35003 ) ;
#16120=CARTESIAN_POINT ( 'NONE',  ( -0.1508021419688995723, 0.4665171419162755795, 0.1089215716836984676 ) ) ;
#16157=FACE_OUTER_BOUND ( 'NONE', #5549, .T. ) ;
#16181=DIRECTION ( 'NONE',  ( -1.000000000000000000, -2.276539994720197063E-15, 0.000000000000000000 ) ) ;
#16198=CARTESIAN_POINT ( 'NONE',  ( -0.1696286242763907215, 0.4941126639394833875, 0.3207424310465851192 ) ) ;
#16205=DIRECTION ( 'NONE',  ( -8.881784197001246407E-16, 2.361472542561082612E-16, -1.000000000000000000 ) ) ;
#16216=EDGE_LOOP ( 'NONE', ( #27990, #24711, #3137, #27115, #21886 ) ) ;
#16268=CARTESIAN_POINT ( 'NONE',  ( -0.1710642718812829255, 0.4986889572247755198, 0.3749999999999999445 ) ) ;
#16286=EDGE_CURVE ( 'NONE', #30856, #36434, #11334, .T. ) ;
#16307=CARTESIAN_POINT ( 'NONE',  ( -0.1743922129835733803, -0.5166151207188712791, 0.3749999999999999445 ) ) ;
#16312=CIRCLE ( 'NONE', #39288, 0.9237847906030155487 ) ;
#16316=CARTESIAN_POINT ( 'NONE',  ( -0.1628171590788634604, 0.5058980335669979178, 0.1333422639292566048 ) ) ;
#16322=CARTESIAN_POINT ( 'NONE',  ( -0.1684323895665170989, 0.5231977504176972271, 0.3102582297535285139 ) ) ;
#16357=DIRECTION ( 'NONE',  ( 8.881784197001246407E-16, -2.361472542561082612E-16, 1.000000000000000000 ) ) ;
#16380=CARTESIAN_POINT ( 'NONE',  ( -0.1628177922134294298, 0.5059000297268239077, 0.3228062255482121445 ) ) ;
#16391=ORIENTED_EDGE ( 'NONE', *, *, #1272, .F. ) ;
#16393=CARTESIAN_POINT ( 'NONE',  ( -0.08408070219615604302, -0.09959325338431369856, 0.09999999999999892308 ) ) ;
#16478=DIRECTION ( 'NONE',  ( -8.881784197001246407E-16, 2.361472542561082612E-16, -1.000000000000000000 ) ) ;
#16483=FACE_OUTER_BOUND ( 'NONE', #19772, .T. ) ;
#16505=CIRCLE ( 'NONE', #21772, 1.991674066779353769 ) ;
#16516=( CONVERSION_BASED_UNIT ( 'INCH', #3156 ) LENGTH_UNIT ( ) NAMED_UNIT ( #32012 ) );
#16544=DIRECTION ( 'NONE',  ( 1.000000000000000000, -3.287861740168050473E-16, -8.266623803851098360E-16 ) ) ;
#16584=CARTESIAN_POINT ( 'NONE',  ( -0.1529745177444770954, 0.4738847129974458894, 0.3606502365071836969 ) ) ;
#16598=ORIENTED_EDGE ( 'NONE', *, *, #28755, .T. ) ;
#16604=CARTESIAN_POINT ( 'NONE',  ( -0.1206014988277990946, -0.5041571071311168328, 0.1364167062886329496 ) ) ;
#16611=TOROIDAL_SURFACE ( 'NONE', #17886, 0.04500000000000032446, 0.01499999999999999944 ) ;
#16641=DIRECTION ( 'NONE',  ( 0.9766636885342073748, -0.2147743920926257488, 0.000000000000000000 ) ) ;
#16706=TOROIDAL_SURFACE ( 'NONE', #17343, 1.971674066779348866, 0.02999999999999999889 ) ;
#16738=DIRECTION ( 'NONE',  ( 1.000000000000000000, 1.450080480853946466E-15, -8.881784197001242463E-16 ) ) ;
#16764=DIRECTION ( 'NONE',  ( -8.881784197001246407E-16, 2.361472542561082612E-16, -1.000000000000000000 ) ) ;
#16799=CARTESIAN_POINT ( 'NONE',  ( -0.1617502512268847170, 0.4682890762661567896, 0.3382895567546961857 ) ) ;
#16808=DIRECTION ( 'NONE',  ( 8.881784197001246407E-16, -2.361472542561082612E-16, 1.000000000000000000 ) ) ;
#16834=DIRECTION ( 'NONE',  ( -8.881784197001246407E-16, 2.361472542561082612E-16, -1.000000000000000000 ) ) ;
#16952=DIRECTION ( 'NONE',  ( -8.881784197001246407E-16, 2.361472542561082612E-16, -1.000000000000000000 ) ) ;
#16985=CARTESIAN_POINT ( 'NONE',  ( -0.1743922129835733803, -0.5166151207188712791, 0.3749999999999999445 ) ) ;
#16992=CARTESIAN_POINT ( 'NONE',  ( -0.1608142870581997230, 0.4995150451154461990, 0.3323678566780360333 ) ) ;
#17033=CARTESIAN_POINT ( 'NONE',  ( -0.1157923916715156154, -0.5295015842444055210, 0.3181161673586314631 ) ) ;
#17058=EDGE_CURVE ( 'NONE', #10109, #35064, #27145, .T. ) ;
#17082=DIRECTION ( 'NONE',  ( 1.776356839400255198E-15, 2.542300904468944507E-15, 1.000000000000000000 ) ) ;
#17118=AXIS2_PLACEMENT_3D ( 'NONE', #38883, #7200, #894 ) ;
#17132=LINE ( 'NONE', #30093, #27019 ) ;
#17137=ORIENTED_EDGE ( 'NONE', *, *, #2383, .F. ) ;
#17141=ORIENTED_EDGE ( 'NONE', *, *, #32786, .T. ) ;
#17169=AXIS2_PLACEMENT_3D ( 'NONE', #32365, #16952, #16544 ) ;
#17223=VECTOR ( 'NONE', #35338, 39.37007874015748143 ) ;
#17266=CIRCLE ( 'NONE', #40243, 0.01500000000000004108 ) ;
#17343=AXIS2_PLACEMENT_3D ( 'NONE', #18665, #31228, #9395 ) ;
#17346=ORIENTED_EDGE ( 'NONE', *, *, #12395, .T. ) ;
#17369=ORIENTED_EDGE ( 'NONE', *, *, #19356, .T. ) ;
#17379=DIRECTION ( 'NONE',  ( -8.881784197001245421E-16, 2.361472542561082612E-16, -1.000000000000000000 ) ) ;
#17394=VERTEX_POINT ( 'NONE', #28409 ) ;
#17424=( BOUNDED_SURFACE ( )  B_SPLINE_SURFACE ( 3, 2, ( 
 ( #27278, #39810, #33620 ),
 ( #8944, #12035, #2774 ),
 ( #28268, #27880, #18205 ),
 ( #2573, #31553, #24805 ) ),
 .UNSPECIFIED., .F., .F., .F. ) 
 B_SPLINE_SURFACE_WITH_KNOTS ( ( 4, 4 ),
 ( 3, 3 ),
 ( 0.0007843053012490898077, 0.001168341556843950548 ),
 ( 0.000000000000000000, 1.000000000000000000 ),
 .UNSPECIFIED. ) 
 GEOMETRIC_REPRESENTATION_ITEM ( )  RATIONAL_B_SPLINE_SURFACE ( (
 ( 1.000000000000000000, 0.9117915798263158678, 1.000000000000000000),
 ( 1.000000000000000000, 0.9032018617293362528, 1.000000000000000000),
 ( 1.000000000000000000, 0.8990088477696482894, 1.000000000000000000),
 ( 1.000000000000000000, 0.8989970956542941982, 1.000000000000000000) ) ) 
 REPRESENTATION_ITEM ( '' )  SURFACE ( )  );
#17454=CARTESIAN_POINT ( 'NONE',  ( -0.1167294259372888832, -0.5331983348239500708, 0.1528658435937002014 ) ) ;
#17542=SHAPE_REPRESENTATION ( 'Parallelogram front_REAR', ( #27819 ), #32382 ) ;
#17555=ORIENTED_EDGE ( 'NONE', *, *, #8249, .F. ) ;
#17557=LINE ( 'NONE', #32570, #14664 ) ;
#17579=CARTESIAN_POINT ( 'NONE',  ( -0.1604632851855414266, 0.4983239941852535271, 0.1050370266831579524 ) ) ;
#17585=DIRECTION ( 'NONE',  ( 0.9591734532964043547, 0.2828184691484104119, 0.000000000000000000 ) ) ;
#17632=CARTESIAN_POINT ( 'NONE',  ( -0.1696273608102604469, 0.4941101834779037527, 0.3212105875170810365 ) ) ;
#17641=EDGE_CURVE ( 'NONE', #17394, #36928, #14580, .T. ) ;
#17694=VERTEX_POINT ( 'NONE', #24883 ) ;
#17704=B_SPLINE_CURVE_WITH_KNOTS ( 'NONE', 3,
 ( #3447, #16604, #22198, #615, #425, #19093 ),
 .UNSPECIFIED., .F., .F.,
 ( 4, 2, 4 ),
 ( 0.0002303018524726760570, 0.0008163183685728757919, 0.001402334884673075554 ),
 .UNSPECIFIED. ) ;
#17762=ORIENTED_EDGE ( 'NONE', *, *, #38938, .T. ) ;
#17783=EDGE_CURVE ( 'NONE', #1249, #9409, #21837, .T. ) ;
#17791=DIRECTION ( 'NONE',  ( -1.000000000000000000, -1.448788479720436272E-15, 8.229804381843897223E-16 ) ) ;
#17886=AXIS2_PLACEMENT_3D ( 'NONE', #9581, #38715, #28292 ) ;
#17957=CIRCLE ( 'NONE', #4184, 0.9087847906030154244 ) ;
#17973=EDGE_CURVE ( 'NONE', #35865, #11425, #32997, .T. ) ;
#17981=CARTESIAN_POINT ( 'NONE',  ( -0.1102510911460846676, -0.5035121463812856080, 0.3528822442262287695 ) ) ;
#18018=VECTOR ( 'NONE', #25529, 39.37007874015748143 ) ;
#18036=CARTESIAN_POINT ( 'NONE',  ( -0.1630570426857087529, 0.4726602372414832054, 0.3374198529391165269 ) ) ;
#18059=CARTESIAN_POINT ( 'NONE',  ( -0.1304423469995336093, -0.5262799683630398073, 0.3749999999999999445 ) ) ;
#18082=CIRCLE ( 'NONE', #4936, 0.03000000000000007175 ) ;
#18105=ORIENTED_EDGE ( 'NONE', *, *, #12296, .T. ) ;
#18106=DIRECTION ( 'NONE',  ( 1.000000000000000000, 1.450080480853946466E-15, -8.881784197001242463E-16 ) ) ;
#18107=CARTESIAN_POINT ( 'NONE',  ( -0.1092363788443093259, -0.4985689912534735369, 0.1005717796975812012 ) ) ;
#18150=ORIENTED_EDGE ( 'NONE', *, *, #31394, .T. ) ;
#18158=VERTEX_POINT ( 'NONE', #31494 ) ;
#18175=CARTESIAN_POINT ( 'NONE',  ( -0.1589779575897145303, 0.4935643744415411649, 0.1021333108076148272 ) ) ;
#18177=CIRCLE ( 'NONE', #32620, 1.986674066779353875 ) ;
#18193=EDGE_CURVE ( 'NONE', #9291, #33568, #4096, .T. ) ;
#18198=EDGE_LOOP ( 'NONE', ( #32314, #25773, #4355, #13893 ) ) ;
#18205=CARTESIAN_POINT ( 'NONE',  ( -0.1167294258596054818, -0.5331983345538300334, 0.1478951491071729685 ) ) ;
#18227=CARTESIAN_POINT ( 'NONE',  ( -0.2900000000000008127, 0.5182417262804733804, 0.3600000000000000422 ) ) ;
#18242=CARTESIAN_POINT ( 'NONE',  ( -0.1707627412572631231, 0.4977336986496899707, 0.3126474374754099061 ) ) ;
#18312=CARTESIAN_POINT ( 'NONE',  ( -0.1127285386967662312, -0.5155187098906055532, 0.1369073159183774313 ) ) ;
#18365=EDGE_LOOP ( 'NONE', ( #38889, #37950, #9821, #34131, #17141, #23687 ) ) ;
#18383=CARTESIAN_POINT ( 'NONE',  ( -0.1873388932668322293, 0.5325605939836577374, 0.3599999999999994316 ) ) ;
#18423=AXIS2_PLACEMENT_3D ( 'NONE', #22325, #28271, #136 ) ;
#18440=FACE_OUTER_BOUND ( 'NONE', #2394, .T. ) ;
#18452=DIRECTION ( 'NONE',  ( -8.881784197001246407E-16, 2.361472542561082612E-16, -1.000000000000000000 ) ) ;
#18478=CARTESIAN_POINT ( 'NONE',  ( -0.1105109110478834505, -0.5048634036869017461, 0.3351973644282421061 ) ) ;
#18479=AXIS2_PLACEMENT_3D ( 'NONE', #22385, #802, #22594 ) ;
#18481=EDGE_CURVE ( 'NONE', #5206, #35865, #37603, .T. ) ;
#18498=AXIS2_PLACEMENT_3D ( 'NONE', #9901, #25758, #7406 ) ;
#18504=CARTESIAN_POINT ( 'NONE',  ( -0.1049931804392591206, -0.4770575742336283231, 0.3602693336304588212 ) ) ;
#18566=VERTEX_POINT ( 'NONE', #4869 ) ;
#18607=VERTEX_POINT ( 'NONE', #2013 ) ;
#18655=DIRECTION ( 'NONE',  ( 1.000000000000000000, 2.276539994720212446E-15, 0.000000000000000000 ) ) ;
#18661=ORIENTED_EDGE ( 'NONE', *, *, #1259, .F. ) ;
#18665=CARTESIAN_POINT ( 'NONE',  ( -2.070754768975509030, -0.09959325338431655739, 0.09550516381870291505 ) ) ;
#18723=ORIENTED_EDGE ( 'NONE', *, *, #8471, .F. ) ;
#18739=AXIS2_PLACEMENT_3D ( 'NONE', #37101, #24174, #39566 ) ;
#18804=CARTESIAN_POINT ( 'NONE',  ( -0.1572280491643790745, 0.4879031095700105403, 0.3568535915792940827 ) ) ;
#18824=ORIENTED_EDGE ( 'NONE', *, *, #7634, .F. ) ;
#18868=CARTESIAN_POINT ( 'NONE',  ( -0.1603938765018536328, 0.4636889572247743230, 0.1178658435936996290 ) ) ;
#18899=EDGE_LOOP ( 'NONE', ( #17369, #28787, #24162, #31063, #28550 ) ) ;
#18900=ORIENTED_EDGE ( 'NONE', *, *, #27504, .T. ) ;
#18989=CARTESIAN_POINT ( 'NONE',  ( -0.1617555154933773554, 0.4683069300263263957, 0.1178658435716314345 ) ) ;
#18998=CARTESIAN_POINT ( 'NONE',  ( -0.1625122179509649878, 0.5048329626761703937, 0.3461446680885723604 ) ) ;
#19032=ORIENTED_EDGE ( 'NONE', *, *, #38499, .F. ) ;
#19039=DIRECTION ( 'NONE',  ( -1.000000000000000000, -2.276539994720197063E-15, 0.000000000000000000 ) ) ;
#19057=MANIFOLD_SOLID_BREP ( 'Fillet2', #14854 ) ;
#19077=DIRECTION ( 'NONE',  ( 1.000000000000000000, 1.445897915516965072E-15, -8.881784197001242463E-16 ) ) ;
#19086=DIRECTION ( 'NONE',  ( 1.000000000000000000, 1.138269997360109379E-15, 0.000000000000000000 ) ) ;
#19093=CARTESIAN_POINT ( 'NONE',  ( -0.1142670043590670176, -0.4723146173917492918, 0.1178658435936998927 ) ) ;
#19194=CARTESIAN_POINT ( 'NONE',  ( -0.1339136704200476757, -0.4685718226220191851, 0.09550516381870235993 ) ) ;
#19201=TOROIDAL_SURFACE ( 'NONE', #31032, 0.9237847906030132172, 0.01499999999999999944 ) ;
#19260=EDGE_CURVE ( 'NONE', #29556, #18607, #10713, .T. ) ;
#19320=DIRECTION ( 'NONE',  ( -0.05576617208936890391, -0.2535907321052872088, -0.9657027879429589401 ) ) ;
#19330=DIRECTION ( 'NONE',  ( -8.881784197001246407E-16, 2.361472542561082612E-16, -1.000000000000000000 ) ) ;
#19349=FACE_OUTER_BOUND ( 'NONE', #27776, .T. ) ;
#19356=EDGE_CURVE ( 'NONE', #25455, #35064, #17266, .T. ) ;
#19363=CARTESIAN_POINT ( 'NONE',  ( -1.019575837292305609, -0.04310840302198155199, 0.3599999999999999867 ) ) ;
#19364=DIRECTION ( 'NONE',  ( -1.000000000000000000, -2.276539994720197063E-15, 5.691349986800492658E-16 ) ) ;
#19367=DIRECTION ( 'NONE',  ( -1.000000000000000000, -2.276539994720197063E-15, 5.691349986800492658E-16 ) ) ;
#19424=CARTESIAN_POINT ( 'NONE',  ( -0.1082158540381434886, -0.4935046016075740338, 0.3575786101922727722 ) ) ;
#19434=DIRECTION ( 'NONE',  ( 0.9480245940703961871, 0.3181970600707375030, -1.138269997360106420E-15 ) ) ;
#19466=DIRECTION ( 'NONE',  ( -8.881784197001246407E-16, 2.361472542561082612E-16, -1.000000000000000000 ) ) ;
#19484=ORIENTED_EDGE ( 'NONE', *, *, #36669, .F. ) ;
#19485=CARTESIAN_POINT ( 'NONE',  ( -0.1508021419688997666, 0.4665171419162779665, 0.3472338286680826669 ) ) ;
#19522=CARTESIAN_POINT ( 'NONE',  ( -0.1450923023275435264, -0.5230583524816332375, 0.3181161673586322403 ) ) ;
#19534=DIRECTION ( 'NONE',  ( -8.881784197001245421E-16, 2.361472542561082612E-16, -1.000000000000000000 ) ) ;
#19555=DIRECTION ( 'NONE',  ( -1.935058995512185017E-14, 1.000000000000000000, -2.162712994984206616E-14 ) ) ;
#19579=FACE_OUTER_BOUND ( 'NONE', #29853, .T. ) ;
#19665=DIRECTION ( 'NONE',  ( 8.881784197001246407E-16, -2.361472542561082612E-16, 1.000000000000000000 ) ) ;
#19668=VERTEX_POINT ( 'NONE', #35539 ) ;
#19669=CARTESIAN_POINT ( 'NONE',  ( -0.1646293987946935988, 0.5114631127588012971, 0.3384789781300959755 ) ) ;
#19684=FACE_BOUND ( 'NONE', #27892, .T. ) ;
#19690=VERTEX_POINT ( 'NONE', #7344 ) ;
#19707=CARTESIAN_POINT ( 'NONE',  ( -0.1212602504510426477, -0.5073146174426373944, 0.3063129689661391875 ) ) ;
#19766=ORIENTED_EDGE ( 'NONE', *, *, #27146, .F. ) ;
#19772=EDGE_LOOP ( 'NONE', ( #6149, #7683, #35000, #1359, #9382, #26782 ) ) ;
#19785=CIRCLE ( 'NONE', #17169, 0.9087847906030154244 ) ;
#19813=AXIS2_PLACEMENT_3D ( 'NONE', #37948, #3185, #22140 ) ;
#19824=ORIENTED_EDGE ( 'NONE', *, *, #7133, .F. ) ;
#19865=VERTEX_POINT ( 'NONE', #11864 ) ;
#19879=AXIS2_PLACEMENT_3D ( 'NONE', #3096, #2885, #11736 ) ;
#20012=AXIS2_PLACEMENT_3D ( 'NONE', #19194, #24773, #21491 ) ;
#20057=EDGE_CURVE ( 'NONE', #35002, #18607, #33729, .T. ) ;
#20063=EDGE_CURVE ( 'NONE', #19690, #31025, #8918, .T. ) ;
#20124=AXIS2_PLACEMENT_3D ( 'NONE', #32022, #9611, #35318 ) ;
#20125=CIRCLE ( 'NONE', #5645, 0.03000000000000010297 ) ;
#20131=DIRECTION ( 'NONE',  ( 6.260484985480596356E-15, -0.9672079024912928480, 0.2539859707905017805 ) ) ;
#20135=TOROIDAL_SURFACE ( 'NONE', #40499, 1.971674066779348866, 0.02999999999999999889 ) ;
#20221=FACE_OUTER_BOUND ( 'NONE', #26360, .T. ) ;
#20223=FACE_OUTER_BOUND ( 'NONE', #21515, .T. ) ;
#20227=EDGE_CURVE ( 'NONE', #22283, #2874, #32584, .T. ) ;
#20236=FACE_OUTER_BOUND ( 'NONE', #8330, .T. ) ;
#20238=ORIENTED_EDGE ( 'NONE', *, *, #37133, .F. ) ;
#20275=DIRECTION ( 'NONE',  ( -8.881784197001246407E-16, 2.361472542561082612E-16, -1.000000000000000000 ) ) ;
#20283=VERTEX_POINT ( 'NONE', #27773 ) ;
#20287=B_SPLINE_CURVE_WITH_KNOTS ( 'NONE', 3,
 ( #34817, #3346, #32148, #3562 ),
 .UNSPECIFIED., .F., .F.,
 ( 4, 4 ),
 ( 1.891967273893909975E-16, 0.0005779611142783052345 ),
 .UNSPECIFIED. ) ;
#20319=CARTESIAN_POINT ( 'NONE',  ( -0.1707605070207437459, 0.4977265752128576248, 0.1434892898517915460 ) ) ;
#20344=DIRECTION ( 'NONE',  ( 1.000000000000000000, 1.445897915516965072E-15, -8.881784197001242463E-16 ) ) ;
#20430=DIRECTION ( 'NONE',  ( -8.881784197001245421E-16, 2.361472542561082612E-16, -1.000000000000000000 ) ) ;
#20446=ADVANCED_FACE ( 'NONE', ( #6554 ), #12747, .F. ) ;
#20454=ORIENTED_EDGE ( 'NONE', *, *, #22503, .T. ) ;
#20462=CARTESIAN_POINT ( 'NONE',  ( -0.1795773455677915076, 0.4580325878418424201, 0.3606502365332835414 ) ) ;
#20500=CARTESIAN_POINT ( 'NONE',  ( -0.1443922129835730761, -0.5166151207188712791, 0.3749999999999999445 ) ) ;
#20517=CARTESIAN_POINT ( 'NONE',  ( -0.1710642718812885599, 0.4986889572247748537, 0.1481991563822706026 ) ) ;
#20559=VECTOR ( 'NONE', #4550, 39.37007874015748143 ) ;
#20600=EDGE_CURVE ( 'NONE', #12135, #5011, #30483, .T. ) ;
#20669=CARTESIAN_POINT ( 'NONE',  ( -0.1873388932668320905, 0.5325605939836577374, 0.3749999999999996669 ) ) ;
#20764=ORIENTED_EDGE ( 'NONE', *, *, #34872, .F. ) ;
#20772=AXIS2_PLACEMENT_3D ( 'NONE', #31825, #34899, #19077 ) ;
#20862=ORIENTED_EDGE ( 'NONE', *, *, #13141, .T. ) ;
#20949=CARTESIAN_POINT ( 'NONE',  ( -0.1743922129835736579, -0.5166151207188712791, 0.3599999999999997091 ) ) ;
#20957=EDGE_CURVE ( 'NONE', #21489, #39928, #27231, .T. ) ;
#20996=CARTESIAN_POINT ( 'NONE',  ( -0.1204846181304667641, -0.5035940506942969686, 0.1366987775887329726 ) ) ;
#21011=ORIENTED_EDGE ( 'NONE', *, *, #4579, .F. ) ;
#21086=CARTESIAN_POINT ( 'NONE',  ( -0.1157923916715200702, -0.5295015842444287246, 0.3181161673586325178 ) ) ;
#21088=EDGE_LOOP ( 'NONE', ( #23338, #15486, #38498, #10775, #36681 ) ) ;
#21147=AXIS2_PLACEMENT_3D ( 'NONE', #29627, #4327, #683 ) ;
#21157=CARTESIAN_POINT ( 'NONE',  ( -0.1509132741912892484, 0.4664843738648666305, 0.09813923389061192382 ) ) ;
#21193=CARTESIAN_POINT ( 'NONE',  ( -0.2666757540196709186, 0.4921670437878968851, 0.1000000000000002970 ) ) ;
#21195=FACE_OUTER_BOUND ( 'NONE', #29140, .T. ) ;
#21276=CARTESIAN_POINT ( 'NONE',  ( -0.1681560115201664318, 0.5223552577131993502, 0.1414989390318069917 ) ) ;
#21295=DIRECTION ( 'NONE',  ( -8.881784197001246407E-16, 2.361472542561082612E-16, -1.000000000000000000 ) ) ;
#21296=AXIS2_PLACEMENT_3D ( 'NONE', #24974, #34029, #11632 ) ;
#21360=CIRCLE ( 'NONE', #18739, 0.03000000000000006481 ) ;
#21383=CARTESIAN_POINT ( 'NONE',  ( -0.1743922129835733803, -0.5166151207188712791, 0.3749999999999999445 ) ) ;
#21395=CARTESIAN_POINT ( 'NONE',  ( -0.1123064544305657775, -0.5135141720357971895, 0.3236707397771451666 ) ) ;
#21421=CARTESIAN_POINT ( 'NONE',  ( -0.1123123235486658822, -0.5135423695149525791, 0.1325268268875365030 ) ) ;
#21489=VERTEX_POINT ( 'NONE', #35056 ) ;
#21491=DIRECTION ( 'NONE',  ( 0.9823333030490233320, -0.1871397384865000069, -5.691349986800536046E-16 ) ) ;
#21496=DIRECTION ( 'NONE',  ( -8.881784197001245421E-16, 2.361472542561082612E-16, -1.000000000000000000 ) ) ;
#21509=DIRECTION ( 'NONE',  ( 1.000000000000000000, 1.441651681710401470E-15, -8.132394101956109642E-16 ) ) ;
#21512=CARTESIAN_POINT ( 'NONE',  ( -0.1210963378865892032, -0.5065302875297106322, 0.3108129518247104150 ) ) ;
#21515=EDGE_LOOP ( 'NONE', ( #32077, #18723, #39967, #4405, #19032 ) ) ;
#21562=ORIENTED_EDGE ( 'NONE', *, *, #2145, .F. ) ;
#21565=DIRECTION ( 'NONE',  ( -8.881784197001246407E-16, 2.361472542561082612E-16, -1.000000000000000000 ) ) ;
#21573=AXIS2_PLACEMENT_3D ( 'NONE', #22339, #6470, #6875 ) ;
#21590=CARTESIAN_POINT ( 'NONE',  ( -0.1112012347075381491, -0.5082045352551866069, 0.3316257441459560806 ) ) ;
#21614=CARTESIAN_POINT ( 'NONE',  ( -0.1171721259116263736, -0.4872713820691137454, 0.1209876223252377009 ) ) ;
#21620=EDGE_LOOP ( 'NONE', ( #7151, #17762, #20862 ) ) ;
#21678=CARTESIAN_POINT ( 'NONE',  ( -0.1680316146028584534, 0.5219773800263004526, 0.3170215181389828829 ) ) ;
#21701=CIRCLE ( 'NONE', #26382, 0.03000000000000002318 ) ;
#21717=CARTESIAN_POINT ( 'NONE',  ( -2.070754768975508586, -0.09959325338431662678, 0.3600000000000021516 ) ) ;
#21718=DIRECTION ( 'NONE',  ( -8.881784197001246407E-16, 2.361472542561082612E-16, -1.000000000000000000 ) ) ;
#21772=AXIS2_PLACEMENT_3D ( 'NONE', #15159, #37372, #40253 ) ;
#21797=ADVANCED_FACE ( 'NONE', ( #37387 ), #9200, .F. ) ;
#21837=CIRCLE ( 'NONE', #8669, 0.01500000000000000812 ) ;
#21860=VECTOR ( 'NONE', #17379, 39.37007874015748143 ) ;
#21885=CARTESIAN_POINT ( 'NONE',  ( -0.1642263571684470513, 0.5103503754387043179, 0.1528658435937215454 ) ) ;
#21886=ORIENTED_EDGE ( 'NONE', *, *, #28710, .F. ) ;
#21909=VECTOR ( 'NONE', #3722, 39.37007874015748143 ) ;
#21950=CIRCLE ( 'NONE', #13384, 0.9237847906030155487 ) ;
#21954=DIRECTION ( 'NONE',  ( 8.881784197001246407E-16, -2.361472542561082612E-16, 1.000000000000000000 ) ) ;
#21959=CIRCLE ( 'NONE', #23259, 1.986674066779353875 ) ;
#21997=EDGE_CURVE ( 'NONE', #8795, #17394, #34878, .T. ) ;
#22041=DIRECTION ( 'NONE',  ( -6.106226635438322318E-15, 2.142487232963740814E-14, 1.000000000000000000 ) ) ;
#22042=AXIS2_PLACEMENT_3D ( 'NONE', #13364, #22041, #19555 ) ;
#22091=DIRECTION ( 'NONE',  ( -8.881784197001246407E-16, 2.361472542561082612E-16, -1.000000000000000000 ) ) ;
#22118=CARTESIAN_POINT ( 'NONE',  ( -0.2300000000000005651, 0.5182417262804733804, 0.08500000000000004774 ) ) ;
#22120=ORIENTED_EDGE ( 'NONE', *, *, #24063, .T. ) ;
#22133=ORIENTED_EDGE ( 'NONE', *, *, #34048, .F. ) ;
#22140=DIRECTION ( 'NONE',  ( 1.000000000000000000, 1.138269997360102476E-15, -8.881784197001243449E-16 ) ) ;
#22150=DIRECTION ( 'NONE',  ( 1.000000000000000000, 1.441651681710401470E-15, -8.317221240636930495E-16 ) ) ;
#22196=FACE_OUTER_BOUND ( 'NONE', #18365, .T. ) ;
#22198=CARTESIAN_POINT ( 'NONE',  ( -0.1196601186823882668, -0.4996350631411420884, 0.1296977380670712998 ) ) ;
#22236=ORIENTED_EDGE ( 'NONE', *, *, #20600, .F. ) ;
#22242=CARTESIAN_POINT ( 'NONE',  ( -0.2789010053595600835, 0.4834754829570387935, 0.3599999999999999867 ) ) ;
#22269=EDGE_LOOP ( 'NONE', ( #8426, #39264, #9669, #36856 ) ) ;
#22283=VERTEX_POINT ( 'NONE', #14675 ) ;
#22284=CYLINDRICAL_SURFACE ( 'NONE', #2928, 0.06000000000000038636 ) ;
#22293=CARTESIAN_POINT ( 'NONE',  ( -0.1699617389507599718, 0.4951775333576751148, 0.1374137075621940374 ) ) ;
#22325=CARTESIAN_POINT ( 'NONE',  ( -0.1743922129835736579, -0.5166151207188712791, 0.3599999999999997091 ) ) ;
#22339=CARTESIAN_POINT ( 'NONE',  ( -0.1304423469995341367, -0.5262799683630398073, 0.3599999999999994316 ) ) ;
#22343=UNCERTAINTY_MEASURE_WITH_UNIT (LENGTH_MEASURE( 1.000000000000000082E-05 ), #16516, 'distance_accuracy_value', 'NONE');
#22383=DIRECTION ( 'NONE',  ( 1.445848444424219201E-15, -1.000000000000000000, -2.361472542561095431E-16 ) ) ;
#22385=CARTESIAN_POINT ( 'NONE',  ( -0.6247879186461524625, 0.2375666616292461675, 0.3749999999999991673 ) ) ;
#22392=ORIENTED_EDGE ( 'NONE', *, *, #11709, .T. ) ;
#22428=ORIENTED_EDGE ( 'NONE', *, *, #14401, .T. ) ;
#22465=EDGE_LOOP ( 'NONE', ( #8014, #36980, #16598, #11530, #36126, #36595 ) ) ;
#22472=CYLINDRICAL_SURFACE ( 'NONE', #8613, 2.001674066779353556 ) ;
#22489=CARTESIAN_POINT ( 'NONE',  ( -0.1623906354757116699, 0.5045448597005526281, 0.1308137833173692033 ) ) ;
#22503=EDGE_CURVE ( 'NONE', #17394, #10276, #23068, .T. ) ;
#22526=CARTESIAN_POINT ( 'NONE',  ( -0.1443922129835735757, -0.5166151207188711680, 0.08499999999999974243 ) ) ;
#22577=CARTESIAN_POINT ( 'NONE',  ( -0.1707812261971866086, 0.4977922652119593505, 0.3123933982393745090 ) ) ;
#22594=DIRECTION ( 'NONE',  ( 1.000000000000000000, 1.445848444424219398E-15, -8.326672684688652360E-16 ) ) ;
#22652=ORIENTED_EDGE ( 'NONE', *, *, #19260, .F. ) ;
#22706=CARTESIAN_POINT ( 'NONE',  ( -0.1593650814506418767, 0.4947962564849443523, 0.1029884207726652623 ) ) ;
#22788=CARTESIAN_POINT ( 'NONE',  ( -0.1679391139942377487, 0.5216964164670698789, 0.3184569295944921774 ) ) ;
#22799=B_SPLINE_CURVE_WITH_KNOTS ( 'NONE', 3,
 ( #14534, #40453, #18242, #17632, #27315, #40031, #27097, #18036, #30179, #5264 ),
 .UNSPECIFIED., .F., .F.,
 ( 4, 2, 2, 2, 4 ),
 ( 0.001421410091499697263, 0.001776295181873945809, 0.002131180272248194355, 0.002486065362622442466, 0.002840950452996691012 ),
 .UNSPECIFIED. ) ;
#22868=EDGE_CURVE ( 'NONE', #25611, #34346, #7859, .T. ) ;
#22918=CARTESIAN_POINT ( 'NONE',  ( -0.1669433606228599432, 0.5138636982738122860, 0.1528658435937006732 ) ) ;
#22935=EDGE_LOOP ( 'NONE', ( #31292, #39165, #22652, #16391, #1896, #22120 ) ) ;
#22978=FACE_OUTER_BOUND ( 'NONE', #28839, .T. ) ;
#23059=CIRCLE ( 'NONE', #18423, 0.06000000000000038636 ) ;
#23067=CARTESIAN_POINT ( 'NONE',  ( -0.06908312040360534145, -0.09959325338431372632, 0.3602693341844387942 ) ) ;
#23068=CIRCLE ( 'NONE', #32879, 0.03000000000000000583 ) ;
#23070=DIRECTION ( 'NONE',  ( 8.881784197001246407E-16, -2.361472542561082612E-16, 1.000000000000000000 ) ) ;
#23101=CYLINDRICAL_SURFACE ( 'NONE', #10004, 2.001674066779353556 ) ;
#23107=DIRECTION ( 'NONE',  ( -8.881784197001246407E-16, 2.361472542561082612E-16, -1.000000000000000000 ) ) ;
#23109=DIRECTION ( 'NONE',  ( 8.881784197001246407E-16, -2.361472542561082612E-16, 1.000000000000000000 ) ) ;
#23112=( NAMED_UNIT ( * ) SI_UNIT ( $, .STERADIAN. ) SOLID_ANGLE_UNIT ( ) );
#23117=ADVANCED_FACE ( 'NONE', ( #16483 ), #22472, .T. ) ;
#23239=DIRECTION ( 'NONE',  ( -6.106226635438322318E-15, 2.142487232963740814E-14, 1.000000000000000000 ) ) ;
#23259=AXIS2_PLACEMENT_3D ( 'NONE', #32948, #23109, #33162 ) ;
#23266=EDGE_CURVE ( 'NONE', #31025, #30141, #27022, .T. ) ;
#23291=ORIENTED_EDGE ( 'NONE', *, *, #4868, .F. ) ;
#23310=AXIS2_PLACEMENT_3D ( 'NONE', #196, #16205, #10225 ) ;
#23338=ORIENTED_EDGE ( 'NONE', *, *, #4579, .T. ) ;
#23398=DIMENSIONAL_EXPONENTS ( 1.000000000000000000, 0.000000000000000000, 0.000000000000000000, 0.000000000000000000, 0.000000000000000000, 0.000000000000000000, 0.000000000000000000 ) ;
#23401=CARTESIAN_POINT ( 'NONE',  ( -0.1688425317846180274, 0.4915896084592928372, 0.3245441658521737716 ) ) ;
#23404=CARTESIAN_POINT ( 'NONE',  ( -0.08408070219616067820, -0.09959325338431368468, 0.08499999999999965916 ) ) ;
#23411=ORIENTED_EDGE ( 'NONE', *, *, #36333, .F. ) ;
#23413=CIRCLE ( 'NONE', #32563, 0.04500000000000044242 ) ;
#23460=VERTEX_POINT ( 'NONE', #25646 ) ;
#23527=CARTESIAN_POINT ( 'NONE',  ( -0.1172100234506837091, -0.4874937943216617331, 0.3357378396897056083 ) ) ;
#23531=EDGE_CURVE ( 'NONE', #10991, #8795, #13903, .T. ) ;
#23574=CARTESIAN_POINT ( 'NONE',  ( -0.1155415985277065405, -0.5283611291160981160, 0.1337613384747777245 ) ) ;
#23589=EDGE_CURVE ( 'NONE', #2842, #2874, #39515, .T. ) ;
#23609=ORIENTED_EDGE ( 'NONE', *, *, #24842, .T. ) ;
#23617=CARTESIAN_POINT ( 'NONE',  ( -0.1696282724551531063, 0.4941130859153644028, 0.1349535128744439594 ) ) ;
#23687=ORIENTED_EDGE ( 'NONE', *, *, #38499, .T. ) ;
#23701=CARTESIAN_POINT ( 'NONE',  ( -0.07908070219616114560, -0.09959325338431368468, 0.1178658435936986715 ) ) ;
#23723=CIRCLE ( 'NONE', #5969, 0.9237847906030155487 ) ;
#23809=DIRECTION ( 'NONE',  ( -8.881784197001246407E-16, 2.361472542561082612E-16, -1.000000000000000000 ) ) ;
#23810=EDGE_CURVE ( 'NONE', #3794, #7197, #15208, .T. ) ;
#23817=CARTESIAN_POINT ( 'NONE',  ( -0.1687956829044073848, 0.4914472887403515400, 0.1310621546645155122 ) ) ;
#23866=DIRECTION ( 'NONE',  ( -8.881784197001246407E-16, 2.361472542561082612E-16, -1.000000000000000000 ) ) ;
#23936=DIRECTION ( 'NONE',  ( -8.881784197001245421E-16, 2.361472542561082612E-16, -1.000000000000000000 ) ) ;
#23938=AXIS2_PLACEMENT_3D ( 'NONE', #7156, #10462, #16641 ) ;
#23963=DIRECTION ( 'NONE',  ( -1.000000000000000000, -1.448788479720435680E-15, 8.315531510821436104E-16 ) ) ;
#23982=CARTESIAN_POINT ( 'NONE',  ( -2.070754768975509919, -0.09959325338431655739, 0.1000000000000005745 ) ) ;
#24016=PRODUCT_DEFINITION_FORMATION_WITH_SPECIFIED_SOURCE ( 'ANY', '', #29493, .NOT_KNOWN. ) ;
#24063=EDGE_CURVE ( 'NONE', #3794, #31075, #30165, .T. ) ;
#24068=TOROIDAL_SURFACE ( 'NONE', #20772, 0.9237847906030132172, 0.01499999999999999944 ) ;
#24102=CARTESIAN_POINT ( 'NONE',  ( -0.1089540792635167732, -0.4972110540767095688, 0.1150843967103700460 ) ) ;
#24145=DIRECTION ( 'NONE',  ( -8.881784197001246407E-16, 2.361472542561082612E-16, -1.000000000000000000 ) ) ;
#24162=ORIENTED_EDGE ( 'NONE', *, *, #24842, .F. ) ;
#24170=EDGE_LOOP ( 'NONE', ( #18150, #28217, #13207, #25323 ) ) ;
#24171=VERTEX_POINT ( 'NONE', #38444 ) ;
#24174=DIRECTION ( 'NONE',  ( -0.1871397384865033653, -0.9823333030490227769, 9.555504051854013858E-17 ) ) ;
#24181=DIRECTION ( 'NONE',  ( 0.9480245940703961871, 0.3181970600707375030, 0.000000000000000000 ) ) ;
#24220=CARTESIAN_POINT ( 'NONE',  ( -0.1532354427637372674, 0.4747053032734181444, 0.3600204025348321402 ) ) ;
#24254=ORIENTED_EDGE ( 'NONE', *, *, #22868, .T. ) ;
#24394=ORIENTED_EDGE ( 'NONE', *, *, #28755, .F. ) ;
#24417=CARTESIAN_POINT ( 'NONE',  ( -0.1533385355407300699, 0.4750492940987078305, 0.3599999999999999867 ) ) ;
#24434=EDGE_LOOP ( 'NONE', ( #203, #31933, #37383 ) ) ;
#24463=CARTESIAN_POINT ( 'NONE',  ( -0.1062892842221577205, -0.4838739999896025101, 0.3472338291022580847 ) ) ;
#24501=CARTESIAN_POINT ( 'NONE',  ( -0.1157923916715204865, -0.5295015842444287246, 0.1380392329925466954 ) ) ;
#24556=EDGE_LOOP ( 'NONE', ( #33426, #29803, #37190, #15707 ) ) ;
#24608=DIRECTION ( 'NONE',  ( 1.000000000000000000, 2.276539994720214024E-15, -1.138269997360107012E-15 ) ) ;
#24645=CIRCLE ( 'NONE', #22042, 0.03000000000000002318 ) ;
#24656=CYLINDRICAL_SURFACE ( 'NONE', #14734, 0.06000000000000045575 ) ;
#24670=DIRECTION ( 'NONE',  ( -8.881784197001246407E-16, 2.361472542561082612E-16, -1.000000000000000000 ) ) ;
#24692=CARTESIAN_POINT ( 'NONE',  ( -0.2300000000000002875, 0.5182417262804733804, 0.1000000000000000194 ) ) ;
#24711=ORIENTED_EDGE ( 'NONE', *, *, #38374, .F. ) ;
#24773=DIRECTION ( 'NONE',  ( -0.1871397384865033098, -0.9823333030490228879, 2.482107064044991629E-16 ) ) ;
#24805=CARTESIAN_POINT ( 'NONE',  ( -0.1167294259372919918, -0.5331983348239598408, 0.1528658435936951776 ) ) ;
#24813=CARTESIAN_POINT ( 'NONE',  ( -0.1574377185082707353, 0.4885537809602767401, 0.1000000000000000194 ) ) ;
#24842=EDGE_CURVE ( 'NONE', #7197, #10109, #23059, .T. ) ;
#24879=CARTESIAN_POINT ( 'NONE',  ( -0.1044436713285783330, -0.4741860147766016054, 0.3606502365330791493 ) ) ;
#24883=CARTESIAN_POINT ( 'NONE',  ( -0.1142670043590668788, -0.4723146173917492918, 0.3382895567580816443 ) ) ;
#24956=CARTESIAN_POINT ( 'NONE',  ( -0.1684323896976702706, 0.5231977508182777958, 0.1451849067762199241 ) ) ;
#24974=CARTESIAN_POINT ( 'NONE',  ( -2.070754768975509474, -0.09959325338431662678, 0.3602693341844405150 ) ) ;
#24999=DIRECTION ( 'NONE',  ( 1.000000000000000000, 7.250402404269733157E-14, -8.188689774234050758E-16 ) ) ;
#25034=FACE_OUTER_BOUND ( 'NONE', #35550, .T. ) ;
#25066=CARTESIAN_POINT ( 'NONE',  ( -0.1142670043590667539, -0.4723146173917426860, 0.3382895567580836982 ) ) ;
#25083=AXIS2_PLACEMENT_3D ( 'NONE', #35913, #24145, #4016 ) ;
#25184=CIRCLE ( 'NONE', #9439, 1.991674066779354213 ) ;
#25202=ORIENTED_EDGE ( 'NONE', *, *, #23531, .F. ) ;
#25214=CARTESIAN_POINT ( 'NONE',  ( -0.1999999999999997891, 0.5182417262804734914, 0.3749999999999999445 ) ) ;
#25232=DIRECTION ( 'NONE',  ( 1.000000000000000000, 1.446659165673942287E-15, -8.266623803851098360E-16 ) ) ;
#25300=DIRECTION ( 'NONE',  ( -1.000000000000000000, -2.276539994720197063E-15, 0.000000000000000000 ) ) ;
#25307=CARTESIAN_POINT ( 'NONE',  ( -0.2666757540196709186, 0.4921670437878968851, 0.3599999999999988765 ) ) ;
#25310=CARTESIAN_POINT ( 'NONE',  ( -1.019575837292305831, -0.04310840302198155199, 0.3750000000000002220 ) ) ;
#25323=ORIENTED_EDGE ( 'NONE', *, *, #12309, .F. ) ;
#25370=EDGE_CURVE ( 'NONE', #9409, #18158, #23723, .T. ) ;
#25410=ORIENTED_EDGE ( 'NONE', *, *, #18481, .T. ) ;
#25429=CARTESIAN_POINT ( 'NONE',  ( -0.1743922129835733803, -0.5166151207188712791, 0.3749999999999999445 ) ) ;
#25455=VERTEX_POINT ( 'NONE', #9402 ) ;
#25464=VERTEX_POINT ( 'NONE', #21157 ) ;
#25488=DIRECTION ( 'NONE',  ( 1.000000000000000000, 1.517693329813464577E-15, -7.588466649067322887E-16 ) ) ;
#25499=CARTESIAN_POINT ( 'NONE',  ( -0.1743922129835733803, -0.5166151207188712791, 0.3749999999999999445 ) ) ;
#25518=CYLINDRICAL_SURFACE ( 'NONE', #39805, 0.06000000000000045575 ) ;
#25529=DIRECTION ( 'NONE',  ( 8.881784197001245421E-16, -2.361472542561082612E-16, 1.000000000000000000 ) ) ;
#25548=ORIENTED_EDGE ( 'NONE', *, *, #39220, .F. ) ;
#25554=DIRECTION ( 'NONE',  ( -8.881784197001246407E-16, 2.361472542561082612E-16, -1.000000000000000000 ) ) ;
#25571=CARTESIAN_POINT ( 'NONE',  ( -0.1638606670177142899, 0.5090623078239778776, 0.1147396705136388417 ) ) ;
#25581=( LENGTH_UNIT ( ) NAMED_UNIT ( * ) SI_UNIT ( $, .METRE. ) );
#25598=ORIENTED_EDGE ( 'NONE', *, *, #1259, .T. ) ;
#25611=VERTEX_POINT ( 'NONE', #797 ) ;
#25646=CARTESIAN_POINT ( 'NONE',  ( -0.2600000000000003419, 0.5182417262804733804, 0.3749999999999999445 ) ) ;
#25649=CARTESIAN_POINT ( 'NONE',  ( -0.1623927644724277586, 0.5045516355107052542, 0.3253307341376578954 ) ) ;
#25676=CIRCLE ( 'NONE', #17118, 0.01499999999999999424 ) ;
#25700=ORIENTED_EDGE ( 'NONE', *, *, #27504, .F. ) ;
#25747=CIRCLE ( 'NONE', #32979, 2.001674066779353556 ) ;
#25758=DIRECTION ( 'NONE',  ( -8.881784197001246407E-16, 2.361472542561082612E-16, -1.000000000000000000 ) ) ;
#25773=ORIENTED_EDGE ( 'NONE', *, *, #31035, .T. ) ;
#25780=CARTESIAN_POINT ( 'NONE',  ( -0.1608166228773026118, 0.4995225507409988275, 0.1237952727409415976 ) ) ;
#25787=SHAPE_REPRESENTATION_RELATIONSHIP ( 'NONE' , 'NONE' ,  #17542, #14726 ) ;
#25796=AXIS2_PLACEMENT_3D ( 'NONE', #38069, #28209, #34984 ) ;
#25831=ORIENTED_EDGE ( 'NONE', *, *, #7908, .T. ) ;
#25853=DIRECTION ( 'NONE',  ( 8.326672684688655318E-16, -2.361472542561083598E-16, 1.000000000000000000 ) ) ;
#25864=CARTESIAN_POINT ( 'NONE',  ( -0.1684323895664757431, 0.5231977504175445715, 0.3032895567580804475 ) ) ;
#25919=VERTEX_POINT ( 'NONE', #24813 ) ;
#25993=CARTESIAN_POINT ( 'NONE',  ( -2.070754768975509474, -0.09959325338431662678, 0.3750000000000004996 ) ) ;
#25998=CYLINDRICAL_SURFACE ( 'NONE', #15448, 0.03000000000000029379 ) ;
#26071=CARTESIAN_POINT ( 'NONE',  ( -0.1665334215456046041, 0.5173690063053929533, 0.3289428497172474652 ) ) ;
#26195=( NAMED_UNIT ( * ) PLANE_ANGLE_UNIT ( ) SI_UNIT ( $, .RADIAN. ) );
#26249=CYLINDRICAL_SURFACE ( 'NONE', #38429, 0.03000000000000029379 ) ;
#26253=CARTESIAN_POINT ( 'NONE',  ( -0.1969433606228592482, 0.5138636982738209458, 0.3032895567580813356 ) ) ;
#26259=CARTESIAN_POINT ( 'NONE',  ( -0.1684323897528365310, 0.5231977509867857812, 0.3108929459560300645 ) ) ;
#26318=AXIS2_PLACEMENT_3D ( 'NONE', #5545, #28378, #18106 ) ;
#26359=EDGE_LOOP ( 'NONE', ( #2112, #18900, #240, #1385 ) ) ;
#26360=EDGE_LOOP ( 'NONE', ( #25700, #33957, #28377, #27302 ) ) ;
#26366=FACE_OUTER_BOUND ( 'NONE', #26359, .T. ) ;
#26372=ORIENTED_EDGE ( 'NONE', *, *, #11709, .F. ) ;
#26382=AXIS2_PLACEMENT_3D ( 'NONE', #4518, #17082, #4717 ) ;
#26405=ORIENTED_EDGE ( 'NONE', *, *, #39675, .F. ) ;
#26456=CARTESIAN_POINT ( 'NONE',  ( -0.1710642717598483409, 0.4986889574318792984, 0.3078512670230422743 ) ) ;
#26461=FACE_OUTER_BOUND ( 'NONE', #15529, .T. ) ;
#26497=CARTESIAN_POINT ( 'NONE',  ( -0.1212602504878793896, -0.5073146173917532087, 0.3032895567580782270 ) ) ;
#26510=ORIENTED_EDGE ( 'NONE', *, *, #11494, .T. ) ;
#26518=CARTESIAN_POINT ( 'NONE',  ( -0.1969433606228599420, 0.5138636982738206127, 0.1528658435937004789 ) ) ;
#26542=CYLINDRICAL_SURFACE ( 'NONE', #12783, 2.001674066779353556 ) ;
#26616=ADVANCED_FACE ( 'NONE', ( #38856 ), #19201, .T. ) ;
#26669=DIRECTION ( 'NONE',  ( -8.881784197001246407E-16, 2.361472542561082612E-16, -1.000000000000000000 ) ) ;
#26704=CARTESIAN_POINT ( 'NONE',  ( -0.1655961216393967705, 0.4810575411953303959, 0.1221435944151030156 ) ) ;
#26757=AXIS2_PLACEMENT_3D ( 'NONE', #33984, #5789, #885 ) ;
#26782=ORIENTED_EDGE ( 'NONE', *, *, #20227, .T. ) ;
#26795=EDGE_CURVE ( 'NONE', #2874, #35762, #11293, .T. ) ;
#26842=EDGE_LOOP ( 'NONE', ( #15435, #34740, #32124, #12001 ) ) ;
#26862=EDGE_CURVE ( 'NONE', #25919, #25464, #29494, .T. ) ;
#26929=DIRECTION ( 'NONE',  ( 1.000000000000000000, 1.446659165673942287E-15, -8.266623803851098360E-16 ) ) ;
#26959=CARTESIAN_POINT ( 'NONE',  ( -0.1053653701217514282, -0.4790241930300290774, 0.1089215720160774531 ) ) ;
#26980=CARTESIAN_POINT ( 'NONE',  ( -0.1710642718812832863, 0.4986889572247755198, 0.3032895567580813356 ) ) ;
#27017=CIRCLE ( 'NONE', #101, 0.06000000000000045575 ) ;
#27019=VECTOR ( 'NONE', #23936, 39.37007874015748143 ) ;
#27022=CIRCLE ( 'NONE', #18498, 0.03000000000000029379 ) ;
#27074=AXIS2_PLACEMENT_3D ( 'NONE', #14365, #21718, #26929 ) ;
#27075=LINE ( 'NONE', #20500, #37104 ) ;
#27097=CARTESIAN_POINT ( 'NONE',  ( -0.1655857493438386840, 0.4810233835288760806, 0.3340284351899800441 ) ) ;
#27115=ORIENTED_EDGE ( 'NONE', *, *, #11494, .F. ) ;
#27130=VERTEX_POINT ( 'NONE', #31849 ) ;
#27145=CIRCLE ( 'NONE', #21147, 0.06000000000000038636 ) ;
#27146=EDGE_CURVE ( 'NONE', #5206, #18566, #28762, .T. ) ;
#27183=CARTESIAN_POINT ( 'NONE',  ( -0.2043922129835741008, -0.5166151207188713901, 0.08499999999999979794 ) ) ;
#27186=ORIENTED_EDGE ( 'NONE', *, *, #1206, .F. ) ;
#27199=CIRCLE ( 'NONE', #39660, 2.001671648589477215 ) ;
#27210=PRODUCT_CONTEXT ( 'NONE', #37659, 'mechanical' ) ;
#27231=CIRCLE ( 'NONE', #23310, 0.9237847906030155487 ) ;
#27254=CARTESIAN_POINT ( 'NONE',  ( -0.2043922129835736845, -0.5166151207188713901, 0.3749999999999999445 ) ) ;
#27278=CARTESIAN_POINT ( 'NONE',  ( -0.1210148435730048905, -0.5061394519556924321, 0.1438724812234762340 ) ) ;
#27281=DIRECTION ( 'NONE',  ( -8.881784197001246407E-16, 2.361472542561082612E-16, -1.000000000000000000 ) ) ;
#27302=ORIENTED_EDGE ( 'NONE', *, *, #39220, .T. ) ;
#27315=CARTESIAN_POINT ( 'NONE',  ( -0.1688017273025826936, 0.4914669153062960483, 0.3250764289764328518 ) ) ;
#27354=DIRECTION ( 'NONE',  ( 1.000000000000000000, 1.450080480853946466E-15, -8.881784197001242463E-16 ) ) ;
#27387=CARTESIAN_POINT ( 'NONE',  ( -0.1157923916714887341, -0.5295015842442657439, 0.1380392329925907435 ) ) ;
#27433=CARTESIAN_POINT ( 'NONE',  ( -0.1731185243557757936, 0.5373335498847187086, 0.3749999999999993894 ) ) ;
#27456=ADVANCED_FACE ( 'NONE', ( #20223 ), #16611, .T. ) ;
#27504=EDGE_CURVE ( 'NONE', #35126, #27130, #32334, .T. ) ;
#27524=DIRECTION ( 'NONE',  ( 1.000000000000000000, 1.138269997360101095E-15, -1.138269997360101095E-15 ) ) ;
#27541=VERTEX_POINT ( 'NONE', #7841 ) ;
#27550=CARTESIAN_POINT ( 'NONE',  ( -0.1204800139379124113, -0.5035717010276916650, 0.3194901984145553375 ) ) ;
#27570=CARTESIAN_POINT ( 'NONE',  ( -0.1061036098701638175, -0.4827967145417200179, 0.3599999999999999867 ) ) ;
#27653=CARTESIAN_POINT ( 'NONE',  ( -0.1138236225804938051, -0.5205343845807006709, 0.3387850541077466748 ) ) ;
#27697=VECTOR ( 'NONE', #19534, 39.37007874015748143 ) ;
#27725=ORIENTED_EDGE ( 'NONE', *, *, #21997, .T. ) ;
#27746=CARTESIAN_POINT ( 'NONE',  ( -0.1124400704934123835, -0.5139941482047849508, 0.3450122074418399687 ) ) ;
#27772=CARTESIAN_POINT ( 'NONE',  ( -0.1068489084554431895, -0.4866459697500206683, 0.09652185631084100881 ) ) ;
#27773=CARTESIAN_POINT ( 'NONE',  ( -0.1212602504878775439, -0.5073146173917505442, 0.3032895567580813356 ) ) ;
#27776=EDGE_LOOP ( 'NONE', ( #28993, #515, #24254, #32199 ) ) ;
#27819=AXIS2_PLACEMENT_3D ( 'NONE', #8920, #2961, #8315 ) ;
#27840=AXIS2_PLACEMENT_3D ( 'NONE', #34485, #25853, #4012 ) ;
#27880=CARTESIAN_POINT ( 'NONE',  ( -0.1126900943766902807, -0.5191528597923980026, 0.1491007326289749135 ) ) ;
#27889=ORIENTED_EDGE ( 'NONE', *, *, #17058, .T. ) ;
#27892=EDGE_LOOP ( 'NONE', ( #30711, #37079 ) ) ;
#27912=AXIS2_PLACEMENT_3D ( 'NONE', #29216, #13769, #19364 ) ;
#27920=CARTESIAN_POINT ( 'NONE',  ( -2.070754768975509919, -0.09959325338431655739, 0.1000000000000005745 ) ) ;
#27963=CARTESIAN_POINT ( 'NONE',  ( -0.2136509456379323546, -0.4946207598421927254, 0.1000000000000000194 ) ) ;
#27990=ORIENTED_EDGE ( 'NONE', *, *, #29028, .F. ) ;
#27999=ORIENTED_EDGE ( 'NONE', *, *, #24063, .F. ) ;
#28001=AXIS2_PLACEMENT_3D ( 'NONE', #35293, #19466, #16181 ) ;
#28045=EDGE_CURVE ( 'NONE', #19865, #4879, #35791, .T. ) ;
#28049=CARTESIAN_POINT ( 'NONE',  ( -0.2136509456379324934, -0.4946207598421927254, 0.08499999999999977018 ) ) ;
#28069=EDGE_CURVE ( 'NONE', #30141, #31025, #34373, .T. ) ;
#28125=DIRECTION ( 'NONE',  ( 8.881784197001246407E-16, -2.361472542561082612E-16, 1.000000000000000000 ) ) ;
#28209=DIRECTION ( 'NONE',  ( 8.881784197001246407E-16, -2.361472542561082612E-16, 1.000000000000000000 ) ) ;
#28217=ORIENTED_EDGE ( 'NONE', *, *, #14499, .F. ) ;
#28239=CARTESIAN_POINT ( 'NONE',  ( -0.1679467284716811559, 0.5217198260998645587, 0.1377606880063828310 ) ) ;
#28268=CARTESIAN_POINT ( 'NONE',  ( -0.1212602505241952427, -0.5073146173415898907, 0.1498414178977066080 ) ) ;
#28271=DIRECTION ( 'NONE',  ( -8.881784197001246407E-16, 2.361472542561082612E-16, -1.000000000000000000 ) ) ;
#28284=DIRECTION ( 'NONE',  ( -8.881784197001246407E-16, 2.361472542561082612E-16, -1.000000000000000000 ) ) ;
#28292=DIRECTION ( 'NONE',  ( 1.000000000000000000, 1.138269997360101095E-15, -8.881784197001243449E-16 ) ) ;
#28377=ORIENTED_EDGE ( 'NONE', *, *, #29103, .T. ) ;
#28378=DIRECTION ( 'NONE',  ( 8.881784197001246407E-16, -2.361472542561082612E-16, 1.000000000000000000 ) ) ;
#28409=CARTESIAN_POINT ( 'NONE',  ( -0.06919656468380704084, -0.09959325338431368468, 0.09813923389047332635 ) ) ;
#28438=FACE_OUTER_BOUND ( 'NONE', #22935, .T. ) ;
#28550=ORIENTED_EDGE ( 'NONE', *, *, #35879, .F. ) ;
#28584=CARTESIAN_POINT ( 'NONE',  ( -0.1157923916715203477, -0.5295015842444287246, 0.3599999999999988765 ) ) ;
#28629=EDGE_CURVE ( 'NONE', #16008, #24171, #10063, .T. ) ;
#28673=CARTESIAN_POINT ( 'NONE',  ( -0.1071618391680946858, -0.4882221650595564011, 0.3591756789878952638 ) ) ;
#28684=DIRECTION ( 'NONE',  ( 0.3181970600707391683, -0.9480245940703956320, -2.369716614345735130E-16 ) ) ;
#28710=EDGE_CURVE ( 'NONE', #34346, #11425, #36362, .T. ) ;
#28741=CARTESIAN_POINT ( 'NONE',  ( -0.2300000000000002875, 0.5182417262804733804, 0.1000000000000000194 ) ) ;
#28755=EDGE_CURVE ( 'NONE', #12063, #5206, #7433, .T. ) ;
#28760=EDGE_CURVE ( 'NONE', #10276, #5846, #25184, .T. ) ;
#28762=LINE ( 'NONE', #28946, #17223 ) ;
#28787=ORIENTED_EDGE ( 'NONE', *, *, #17058, .F. ) ;
#28839=EDGE_LOOP ( 'NONE', ( #18824, #40273, #2999, #24394 ) ) ;
#28848=CARTESIAN_POINT ( 'NONE',  ( -2.070754768975508586, -0.09959325338431662678, 0.3600000000000021516 ) ) ;
#28852=CARTESIAN_POINT ( 'NONE',  ( -0.1638686671686519769, 0.5092269732921813619, 0.1413937977834208159 ) ) ;
#28867=CARTESIAN_POINT ( 'NONE',  ( -0.1061036098701638175, -0.4827967145417200179, 0.3599999999999999867 ) ) ;
#28911=FACE_BOUND ( 'NONE', #145, .T. ) ;
#28920=CARTESIAN_POINT ( 'NONE',  ( -0.1638630105338990950, 0.5092090815894948497, 0.3148090297061075793 ) ) ;
#28926=DIRECTION ( 'NONE',  ( 1.000000000000000000, 1.138269997360101095E-15, -8.881784197001243449E-16 ) ) ;
#28945=TOROIDAL_SURFACE ( 'NONE', #26318, 1.986674066779348768, 0.01499999999999999944 ) ;
#28946=CARTESIAN_POINT ( 'NONE',  ( -0.2789010053595598060, 0.4834754829570387935, 0.3749999999999999445 ) ) ;
#28959=CARTESIAN_POINT ( 'NONE',  ( -0.1129900121204313601, -0.5167580615070225258, 0.3146079272632537616 ) ) ;
#28993=ORIENTED_EDGE ( 'NONE', *, *, #17973, .F. ) ;
#29028=EDGE_CURVE ( 'NONE', #10991, #34346, #12066, .T. ) ;
#29046=CARTESIAN_POINT ( 'NONE',  ( -0.09908070219615519592, -0.09959325338431371244, 0.09550516381870127747 ) ) ;
#29048=FACE_OUTER_BOUND ( 'NONE', #24434, .T. ) ;
#29096=CARTESIAN_POINT ( 'NONE',  ( -1.019575837292305609, -0.04310840302198148261, 0.08500000000000004774 ) ) ;
#29103=EDGE_CURVE ( 'NONE', #23460, #4891, #17557, .T. ) ;
#29140=EDGE_LOOP ( 'NONE', ( #12034, #33748, #8742, #37016, #23291 ) ) ;
#29173=CARTESIAN_POINT ( 'NONE',  ( -0.1167294260180564980, -0.5331983351047929753, 0.3082670712249074296 ) ) ;
#29216=CARTESIAN_POINT ( 'NONE',  ( -0.2300000000000005651, 0.5182417262804733804, 0.08500000000000004774 ) ) ;
#29234=DIRECTION ( 'NONE',  ( 1.000000000000000000, 1.445897915516965072E-15, -8.881784197001242463E-16 ) ) ;
#29251=FACE_OUTER_BOUND ( 'NONE', #37783, .T. ) ;
#29316=ORIENTED_EDGE ( 'NONE', *, *, #19356, .F. ) ;
#29347=CARTESIAN_POINT ( 'NONE',  ( -0.1524914371963946857, 0.4722463545162148280, 0.3472338286530670115 ) ) ;
#29402=EDGE_LOOP ( 'NONE', ( #664, #10712, #21011, #38351, #8698, #36939 ) ) ;
#29490=EDGE_LOOP ( 'NONE', ( #22236, #20238, #1596, #34741, #23411, #5768 ) ) ;
#29492=B_SPLINE_CURVE_WITH_KNOTS ( 'NONE', 3,
 ( #36577, #10664, #39051, #17454 ),
 .UNSPECIFIED., .F., .F.,
 ( 4, 4 ),
 ( 2.100114060352324785E-15, 0.0003951776346070152404 ),
 .UNSPECIFIED. ) ;
#29493=PRODUCT ( 'Parallelogram front_REAR', 'Parallelogram front_REAR', '', ( #27210 ) ) ;
#29494=B_SPLINE_CURVE_WITH_KNOTS ( 'NONE', 3,
 ( #39276, #30029, #5298, #14574 ),
 .UNSPECIFIED., .F., .F.,
 ( 4, 4 ),
 ( -1.150894640811756038E-05, 0.0005747792170237640656 ),
 .UNSPECIFIED. ) ;
#29533=CARTESIAN_POINT ( 'NONE',  ( -0.1603938765018607104, 0.4636889572247930857, 0.3382895567580836982 ) ) ;
#29541=EDGE_CURVE ( 'NONE', #5190, #33568, #12090, .T. ) ;
#29556=VERTEX_POINT ( 'NONE', #18059 ) ;
#29606=DIRECTION ( 'NONE',  ( -8.881784197001246407E-16, 2.361472542561082612E-16, -1.000000000000000000 ) ) ;
#29627=CARTESIAN_POINT ( 'NONE',  ( -0.1743922129835736579, -0.5166151207188712791, 0.3599999999999997091 ) ) ;
#29648=DIRECTION ( 'NONE',  ( -8.881784197001246407E-16, 2.361472542561082612E-16, -1.000000000000000000 ) ) ;
#29699=ORIENTED_EDGE ( 'NONE', *, *, #14816, .T. ) ;
#29761=ADVANCED_FACE ( 'NONE', ( #25034 ), #24656, .T. ) ;
#29767=ADVANCED_FACE ( 'NONE', ( #15376 ), #16706, .T. ) ;
#29803=ORIENTED_EDGE ( 'NONE', *, *, #14401, .F. ) ;
#29853=EDGE_LOOP ( 'NONE', ( #27186, #14152, #25831, #18661 ) ) ;
#29912=CARTESIAN_POINT ( 'NONE',  ( -0.1795773455677817376, 0.4580325878418074481, 0.09550516381870181870 ) ) ;
#30014=ADVANCED_FACE ( 'NONE', ( #26461 ), #36109, .T. ) ;
#30029=CARTESIAN_POINT ( 'NONE',  ( -0.1552051794442718957, 0.4812910476514236646, 0.09878871670238409397 ) ) ;
#30047=CARTESIAN_POINT ( 'NONE',  ( -2.070754768975509474, -0.09959325338431662678, 0.3750000000000004996 ) ) ;
#30093=CARTESIAN_POINT ( 'NONE',  ( -0.2267371898560520127, -0.4872893062166341327, 0.3749999999999996669 ) ) ;
#30116=DIRECTION ( 'NONE',  ( -8.881784197001246407E-16, 2.361472542561082612E-16, -1.000000000000000000 ) ) ;
#30141=VERTEX_POINT ( 'NONE', #22526 ) ;
#30165=B_SPLINE_CURVE_WITH_KNOTS ( 'NONE', 3,
 ( #27570, #40093, #18504, #37018 ),
 .UNSPECIFIED., .F., .F.,
 ( 4, 4 ),
 ( -2.702335329567562820E-05, 0.0001957598036967008186 ),
 .UNSPECIFIED. ) ;
#30179=CARTESIAN_POINT ( 'NONE',  ( -0.1617138679863671380, 0.4681656832120512646, 0.3382895567580770924 ) ) ;
#30233=CARTESIAN_POINT ( 'NONE',  ( -0.1142670043590607726, -0.4723146173917092128, 0.1178658435936972976 ) ) ;
#30272=EDGE_CURVE ( 'NONE', #25464, #5846, #33787, .T. ) ;
#30273=SHAPE_DEFINITION_REPRESENTATION ( #32772, #17542 ) ;
#30336=CARTESIAN_POINT ( 'NONE',  ( -2.070754768975509474, -0.09959325338431662678, 0.3602693341844405150 ) ) ;
#30351=VECTOR ( 'NONE', #35989, 39.37007874015748143 ) ;
#30401=DIRECTION ( 'NONE',  ( -8.881784197001245421E-16, 2.361472542561082612E-16, -1.000000000000000000 ) ) ;
#30454=CARTESIAN_POINT ( 'NONE',  ( -0.1208103506584077974, -0.5051587313117239519, 0.1401839043133216722 ) ) ;
#30478=CARTESIAN_POINT ( 'NONE',  ( -0.09579104668929019906, -0.04310840302198021973, 0.3749999999999993894 ) ) ;
#30483=CIRCLE ( 'NONE', #1605, 0.03000000000000002318 ) ;
#30573=DIRECTION ( 'NONE',  ( 1.445848444424219201E-15, -1.000000000000000000, -2.361472542561095431E-16 ) ) ;
#30580=ADVANCED_FACE ( 'NONE', ( #29251 ), #22284, .T. ) ;
#30636=CARTESIAN_POINT ( 'NONE',  ( -0.1081899703030416854, -0.4934552128794481574, 0.3439540350797968271 ) ) ;
#30677=ORIENTED_EDGE ( 'NONE', *, *, #39561, .T. ) ;
#30700=ADVANCED_FACE ( 'NONE', ( #26366 ), #36216, .F. ) ;
#30711=ORIENTED_EDGE ( 'NONE', *, *, #6623, .T. ) ;
#30802=EDGE_LOOP ( 'NONE', ( #34030, #33917 ) ) ;
#30826=ORIENTED_EDGE ( 'NONE', *, *, #32898, .F. ) ;
#30856=VERTEX_POINT ( 'NONE', #24501 ) ;
#30886=CARTESIAN_POINT ( 'NONE',  ( -0.1210148435730249716, -0.5061394519557976812, 0.3122829191278992389 ) ) ;
#30920=AXIS2_PLACEMENT_3D ( 'NONE', #16393, #22383, #19086 ) ;
#30931=CARTESIAN_POINT ( 'NONE',  ( -0.1112019842995564389, -0.5080904053907916440, 0.3498664773290697805 ) ) ;
#30986=CARTESIAN_POINT ( 'NONE',  ( -0.2300000000000002875, 0.5182417262804733804, 0.1000000000000000194 ) ) ;
#31011=ORIENTED_EDGE ( 'NONE', *, *, #26862, .T. ) ;
#31025=VERTEX_POINT ( 'NONE', #27183 ) ;
#31032=AXIS2_PLACEMENT_3D ( 'NONE', #19363, #38258, #38060 ) ;
#31033=CARTESIAN_POINT ( 'NONE',  ( -0.1093417548588324489, -0.4991680509866276982, 0.3564048400776990699 ) ) ;
#31035=EDGE_CURVE ( 'NONE', #5011, #35762, #24645, .T. ) ;
#31063=ORIENTED_EDGE ( 'NONE', *, *, #1272, .T. ) ;
#31075=VERTEX_POINT ( 'NONE', #35930 ) ;
#31146=CARTESIAN_POINT ( 'NONE',  ( -0.1508044614562676355, 0.4665164580004940720, 0.3602693336111439382 ) ) ;
#31161=ORIENTED_EDGE ( 'NONE', *, *, #35682, .F. ) ;
#31207=DIRECTION ( 'NONE',  ( 8.881784197001246407E-16, -2.361472542561082612E-16, 1.000000000000000000 ) ) ;
#31228=DIRECTION ( 'NONE',  ( 8.881784197001246407E-16, -2.361472542561082612E-16, 1.000000000000000000 ) ) ;
#31276=EDGE_CURVE ( 'NONE', #11981, #30141, #27075, .T. ) ;
#31292=ORIENTED_EDGE ( 'NONE', *, *, #13242, .T. ) ;
#31347=CARTESIAN_POINT ( 'NONE',  ( -0.1650539334306630468, 0.4792632177816705807, 0.1214379789123950643 ) ) ;
#31394=EDGE_CURVE ( 'NONE', #4879, #20283, #18082, .T. ) ;
#31466=FACE_OUTER_BOUND ( 'NONE', #15037, .T. ) ;
#31477=CARTESIAN_POINT ( 'NONE',  ( -0.2300000000000000655, 0.5182417262804733804, 0.3749999999999999445 ) ) ;
#31494=CARTESIAN_POINT ( 'NONE',  ( -0.09579104668929026845, -0.04310840302198015034, 0.08499999999999910405 ) ) ;
#31522=CARTESIAN_POINT ( 'NONE',  ( -0.1583356623530634000, 0.4914777262839043481, 0.1012105261661027239 ) ) ;
#31553=CARTESIAN_POINT ( 'NONE',  ( -0.1126900943574667274, -0.5191528599708484792, 0.1528658435936963711 ) ) ;
#31606=ADVANCED_FACE ( 'NONE', ( #28438 ), #34524, .T. ) ;
#31630=VECTOR ( 'NONE', #20430, 39.37007874015748143 ) ;
#31731=CARTESIAN_POINT ( 'NONE',  ( -0.1588702854552091759, 0.4932535771925591894, 0.1179163363090176136 ) ) ;
#31818=CARTESIAN_POINT ( 'NONE',  ( -0.1574156176409216568, 0.4885425907994525030, 0.3417174393643538921 ) ) ;
#31825=CARTESIAN_POINT ( 'NONE',  ( -1.019575837292305609, -0.04310840302198155199, 0.3599999999999999867 ) ) ;
#31844=CIRCLE ( 'NONE', #20012, 0.03000000000000006481 ) ;
#31849=CARTESIAN_POINT ( 'NONE',  ( -0.2000000000000003164, 0.5182417262804734914, 0.08500000000000001998 ) ) ;
#31933=ORIENTED_EDGE ( 'NONE', *, *, #39124, .T. ) ;
#31943=CARTESIAN_POINT ( 'NONE',  ( -0.1508021419688942433, 0.4665171419162573718, 0.09550516381870209626 ) ) ;
#32012=DIMENSIONAL_EXPONENTS ( 1.000000000000000000, 0.000000000000000000, 0.000000000000000000, 0.000000000000000000, 0.000000000000000000, 0.000000000000000000, 0.000000000000000000 ) ;
#32014=CARTESIAN_POINT ( 'NONE',  ( -0.1613545236348471745, 0.5011730501304613172, 0.3493272269784281070 ) ) ;
#32022=CARTESIAN_POINT ( 'NONE',  ( -0.1969433606228568612, 0.5138636982738121750, 0.3749999999999991673 ) ) ;
#32058=FACE_OUTER_BOUND ( 'NONE', #24170, .T. ) ;
#32077=ORIENTED_EDGE ( 'NONE', *, *, #39120, .F. ) ;
#32112=CARTESIAN_POINT ( 'NONE',  ( -1.019575837292306053, -0.04310840302198148261, 0.09999999999999975575 ) ) ;
#32124=ORIENTED_EDGE ( 'NONE', *, *, #20063, .T. ) ;
#32148=CARTESIAN_POINT ( 'NONE',  ( -0.1073276781670975538, -0.4890918960634570989, 0.09878957693462706025 ) ) ;
#32199=ORIENTED_EDGE ( 'NONE', *, *, #28710, .T. ) ;
#32298=DIRECTION ( 'NONE',  ( 8.881784197001246407E-16, -2.361472542561082612E-16, 1.000000000000000000 ) ) ;
#32314=ORIENTED_EDGE ( 'NONE', *, *, #12395, .F. ) ;
#32331=CARTESIAN_POINT ( 'NONE',  ( -0.1210148435730035998, -0.5061394519556905447, 0.1438724812234790928 ) ) ;
#32334=LINE ( 'NONE', #25214, #20559 ) ;
#32363=AXIS2_PLACEMENT_3D ( 'NONE', #10487, #6786, #19367 ) ;
#32365=CARTESIAN_POINT ( 'NONE',  ( -1.019575837292306053, -0.04310840302198148261, 0.09999999999999975575 ) ) ;
#32382=( GEOMETRIC_REPRESENTATION_CONTEXT ( 3 ) GLOBAL_UNCERTAINTY_ASSIGNED_CONTEXT ( ( #22343 ) ) GLOBAL_UNIT_ASSIGNED_CONTEXT ( ( #16516, #15698, #3954 ) ) REPRESENTATION_CONTEXT ( 'NONE', 'WORKASPACE' ) );
#32410=CARTESIAN_POINT ( 'NONE',  ( -0.1659631349965166869, 0.5156080474714462847, 0.3322463110352252280 ) ) ;
#32416=ADVANCED_FACE ( 'NONE', ( #21195 ), #36645, .T. ) ;
#32435=VECTOR ( 'NONE', #5422, 39.37007874015748143 ) ;
#32450=CARTESIAN_POINT ( 'NONE',  ( -0.1167294259372914089, -0.5331983348239582865, 0.3032895567580760066 ) ) ;
#32555=B_SPLINE_CURVE_WITH_KNOTS ( 'NONE', 3,
 ( #10637, #7547, #7753, #26704, #7942, #23817, #23617, #20319, #20517, #8156 ),
 .UNSPECIFIED., .F., .F.,
 ( 4, 2, 2, 2, 4 ),
 ( 7.269816092100765919E-18, 0.0003553525228749304958, 0.0007107050457498537274, 0.001066057568624777067, 0.001421410091499700299 ),
 .UNSPECIFIED. ) ;
#32563=AXIS2_PLACEMENT_3D ( 'NONE', #12940, #16834, #25488 ) ;
#32570=CARTESIAN_POINT ( 'NONE',  ( -0.2600000000000003419, 0.5182417262804733804, 0.3749999999999999445 ) ) ;
#32584=B_SPLINE_CURVE_WITH_KNOTS ( 'NONE', 3,
 ( #2959, #323, #18804, #37491, #18998, #9312, #35024, #21678, #16322, #34816 ),
 .UNSPECIFIED., .F., .F.,
 ( 4, 2, 2, 2, 4 ),
 ( 0.0002266766535735069562, 0.0007552434839518312520, 0.001283810314330155683, 0.001812377144708480006, 0.002340943975086804112 ),
 .UNSPECIFIED. ) ;
#32620=AXIS2_PLACEMENT_3D ( 'NONE', #33250, #23809, #1810 ) ;
#32623=CARTESIAN_POINT ( 'NONE',  ( -0.1642263571684461076, 0.5103503754387049840, 0.3032895567580806140 ) ) ;
#32633=ORIENTED_EDGE ( 'NONE', *, *, #12329, .F. ) ;
#32679=DIRECTION ( 'NONE',  ( -2.276539994720217574E-15, 1.000000000000000000, -2.162712994984206616E-14 ) ) ;
#32683=DIRECTION ( 'NONE',  ( 8.881784197001246407E-16, -2.361472542561082612E-16, 1.000000000000000000 ) ) ;
#32772=PRODUCT_DEFINITION_SHAPE ( 'NONE', 'NONE',  #6386 ) ;
#32786=EDGE_CURVE ( 'NONE', #18607, #1427, #21959, .T. ) ;
#32810=ORIENTED_EDGE ( 'NONE', *, *, #18193, .F. ) ;
#32851=CARTESIAN_POINT ( 'NONE',  ( -0.1126900943574667691, -0.5191528599708477021, 0.3032895567580773388 ) ) ;
#32879=AXIS2_PLACEMENT_3D ( 'NONE', #29046, #914, #9305 ) ;
#32898=EDGE_CURVE ( 'NONE', #40308, #36434, #37240, .T. ) ;
#32902=( BOUNDED_SURFACE ( )  B_SPLINE_SURFACE ( 3, 2, ( 
 ( #26497, #32851, #32450 ),
 ( #19707, #6953, #29173 ),
 ( #13727, #4654, #39032 ),
 ( #4059, #28959, #17033 ) ),
 .UNSPECIFIED., .F., .F., .F. ) 
 B_SPLINE_SURFACE_WITH_KNOTS ( ( 4, 4 ),
 ( 3, 3 ),
 ( 0.001168341556843763198, 0.001551611072815416289 ),
 ( 0.000000000000000000, 1.000000000000000000 ),
 .UNSPECIFIED. ) 
 GEOMETRIC_REPRESENTATION_ITEM ( )  RATIONAL_B_SPLINE_SURFACE ( (
 ( 1.000000000000000000, 0.8989970956543047453, 1.000000000000000000),
 ( 1.000000000000000000, 0.8989738193133397504, 1.000000000000000000),
 ( 1.000000000000000000, 0.9033319494950228234, 1.000000000000000000),
 ( 1.000000000000000000, 0.9117915798252440585, 1.000000000000000000) ) ) 
 REPRESENTATION_ITEM ( '' )  SURFACE ( )  );
#32931=ORIENTED_EDGE ( 'NONE', *, *, #32898, .T. ) ;
#32948=CARTESIAN_POINT ( 'NONE',  ( -2.070754768975509474, -0.09959325338431662678, 0.3750000000000004996 ) ) ;
#32967=DIRECTION ( 'NONE',  ( 8.881784197001246407E-16, -2.361472542561082612E-16, 1.000000000000000000 ) ) ;
#32979=AXIS2_PLACEMENT_3D ( 'NONE', #21717, #28284, #24999 ) ;
#32997=LINE ( 'NONE', #4803, #21860 ) ;
#33033=DIRECTION ( 'NONE',  ( -8.881784197001245421E-16, 2.361472542561082612E-16, -1.000000000000000000 ) ) ;
#33049=AXIS2_PLACEMENT_3D ( 'NONE', #19522, #19320, #20131 ) ;
#33076=FACE_OUTER_BOUND ( 'NONE', #22269, .T. ) ;
#33083=CARTESIAN_POINT ( 'NONE',  ( -1.019575837292305609, -0.04310840302198148261, 0.08500000000000004774 ) ) ;
#33162=DIRECTION ( 'NONE',  ( 1.000000000000000000, 1.443840457432242888E-15, -8.250516899612815800E-16 ) ) ;
#33182=DIRECTION ( 'NONE',  ( 1.000000000000000000, 1.450080480853946466E-15, -8.359287477863926836E-16 ) ) ;
#33250=CARTESIAN_POINT ( 'NONE',  ( -2.070754768975509474, -0.09959325338431655739, 0.08500000000000142164 ) ) ;
#33313=AXIS2_PLACEMENT_3D ( 'NONE', #32112, #23070, #29234 ) ;
#33356=CARTESIAN_POINT ( 'NONE',  ( -0.1211772861969197951, -0.5069185045468647122, 0.1468025672055963127 ) ) ;
#33360=CARTESIAN_POINT ( 'NONE',  ( -0.2666757540196706411, 0.4921670437878968851, 0.08500000000000004774 ) ) ;
#33426=ORIENTED_EDGE ( 'NONE', *, *, #22503, .F. ) ;
#33456=DIRECTION ( 'NONE',  ( 1.000000000000000000, 1.517693329813464577E-15, -1.517693329813464577E-15 ) ) ;
#33471=DIRECTION ( 'NONE',  ( 1.000000000000000000, 1.138269997360102476E-15, -8.881784197001243449E-16 ) ) ;
#33551=CARTESIAN_POINT ( 'NONE',  ( -0.1196588179077745229, -0.4996288669916953418, 0.3264677846082036927 ) ) ;
#33568=VERTEX_POINT ( 'NONE', #37602 ) ;
#33606=CARTESIAN_POINT ( 'NONE',  ( -0.1157923916715200702, -0.5295015842444287246, 0.3181161673586325178 ) ) ;
#33611=CARTESIAN_POINT ( 'NONE',  ( -0.1669433606228567790, 0.5138636982738122860, 0.3749999999999991673 ) ) ;
#33614=DIRECTION ( 'NONE',  ( -1.000000000000000000, -2.276539994720197063E-15, 0.000000000000000000 ) ) ;
#33620=CARTESIAN_POINT ( 'NONE',  ( -0.1157923916714455881, -0.5295015842440863318, 0.1380392329925437811 ) ) ;
#33703=AXIS2_PLACEMENT_3D ( 'NONE', #30047, #32298, #7396 ) ;
#33712=CARTESIAN_POINT ( 'NONE',  ( -2.070754768975509919, -0.09959325338431655739, 0.09813923389047504720 ) ) ;
#33729=CIRCLE ( 'NONE', #38985, 0.01500000000000000291 ) ;
#33733=CARTESIAN_POINT ( 'NONE',  ( -0.1124521194441292365, -0.5140518175047488203, 0.1111873348898323038 ) ) ;
#33748=ORIENTED_EDGE ( 'NONE', *, *, #39561, .F. ) ;
#33787=CIRCLE ( 'NONE', #35108, 0.03000000000000008563 ) ;
#33813=CARTESIAN_POINT ( 'NONE',  ( -0.1663058949916037810, 0.5166728756553465862, 0.1255325300626441154 ) ) ;
#33886=AXIS2_PLACEMENT_3D ( 'NONE', #28741, #16808, #28926 ) ;
#33910=FACE_OUTER_BOUND ( 'NONE', #16216, .T. ) ;
#33917=ORIENTED_EDGE ( 'NONE', *, *, #28069, .F. ) ;
#33923=VERTEX_POINT ( 'NONE', #33360 ) ;
#33953=DIRECTION ( 'NONE',  ( 0.5794373887239211429, -0.8150167559926626559, 5.038681971366855054E-15 ) ) ;
#33954=CARTESIAN_POINT ( 'NONE',  ( -0.1148699535791915805, -0.5253002637279400311, 0.1262353127152416599 ) ) ;
#33957=ORIENTED_EDGE ( 'NONE', *, *, #6623, .F. ) ;
#33984=CARTESIAN_POINT ( 'NONE',  ( -0.2300000000000000655, 0.5182417262804733804, 0.3749999999999999445 ) ) ;
#34029=DIRECTION ( 'NONE',  ( 8.881784197001246407E-16, -2.361472542561082612E-16, 1.000000000000000000 ) ) ;
#34030=ORIENTED_EDGE ( 'NONE', *, *, #23266, .F. ) ;
#34034=ORIENTED_EDGE ( 'NONE', *, *, #15299, .T. ) ;
#34048=EDGE_CURVE ( 'NONE', #17694, #16008, #34750, .T. ) ;
#34088=CARTESIAN_POINT ( 'NONE',  ( -0.2300000000000000655, 0.5182417262804733804, 0.3749999999999999445 ) ) ;
#34131=ORIENTED_EDGE ( 'NONE', *, *, #19260, .T. ) ;
#34277=CYLINDRICAL_SURFACE ( 'NONE', #40370, 0.03000000000000008910 ) ;
#34346=VERTEX_POINT ( 'NONE', #9837 ) ;
#34373=CIRCLE ( 'NONE', #32363, 0.03000000000000029379 ) ;
#34379=AXIS2_PLACEMENT_3D ( 'NONE', #27920, #11673, #36752 ) ;
#34386=AXIS2_PLACEMENT_3D ( 'NONE', #23982, #2561, #2762 ) ;
#34404=AXIS2_PLACEMENT_3D ( 'NONE', #35261, #28684, #19434 ) ;
#34413=CARTESIAN_POINT ( 'NONE',  ( -0.1710642718812869778, 0.4986889572247778513, 0.1528658435937169657 ) ) ;
#34433=EDGE_LOOP ( 'NONE', ( #13994, #7819, #14960, #7631, #25598, #1482 ) ) ;
#34464=DIRECTION ( 'NONE',  ( 8.881784197001246407E-16, -2.361472542561082612E-16, 1.000000000000000000 ) ) ;
#34481=DIRECTION ( 'NONE',  ( 1.000000000000000000, 1.446659165673942287E-15, -8.266623803851098360E-16 ) ) ;
#34485=CARTESIAN_POINT ( 'NONE',  ( -0.6247879186461532397, 0.2375666616292463063, 0.08499999999999977018 ) ) ;
#34524=TOROIDAL_SURFACE ( 'NONE', #6263, 1.986674066779348768, 0.01499999999999999944 ) ;
#34607=ORIENTED_EDGE ( 'NONE', *, *, #20057, .F. ) ;
#34611=DIRECTION ( 'NONE',  ( -1.000000000000000000, -1.138269997360102279E-15, 1.138269997360102279E-15 ) ) ;
#34711=PLANE ( 'NONE',  #18479 ) ;
#34734=DIRECTION ( 'NONE',  ( 1.000000000000000000, 3.414809992080303089E-15, -1.138269997360101095E-15 ) ) ;
#34740=ORIENTED_EDGE ( 'NONE', *, *, #1297, .F. ) ;
#34741=ORIENTED_EDGE ( 'NONE', *, *, #26862, .F. ) ;
#34750=B_SPLINE_CURVE_WITH_KNOTS ( 'NONE', 3,
 ( #10970, #7846, #23527, #33551, #12172, #30886 ),
 .UNSPECIFIED., .F., .F.,
 ( 4, 2, 4 ),
 ( 0.002802047142276810777, 0.003388785079928765924, 0.003975523017580721505 ),
 .UNSPECIFIED. ) ;
#34807=CARTESIAN_POINT ( 'NONE',  ( -0.1646294012188481148, 0.5114631038222671178, 0.1176773486970680294 ) ) ;
#34816=CARTESIAN_POINT ( 'NONE',  ( -0.1684323895664525950, 0.5231977504174881721, 0.3032895567580808360 ) ) ;
#34817=CARTESIAN_POINT ( 'NONE',  ( -0.1045574869087419617, -0.4741643323009803734, 0.09813923389047396473 ) ) ;
#34872=EDGE_CURVE ( 'NONE', #33568, #2775, #6129, .T. ) ;
#34873=VECTOR ( 'NONE', #30401, 39.37007874015748143 ) ;
#34878=CIRCLE ( 'NONE', #30920, 0.01500000000000000291 ) ;
#34884=DIRECTION ( 'NONE',  ( 8.881784197001246407E-16, -2.361472542561082612E-16, 1.000000000000000000 ) ) ;
#34899=DIRECTION ( 'NONE',  ( 8.881784197001246407E-16, -2.361472542561082612E-16, 1.000000000000000000 ) ) ;
#34912=FACE_BOUND ( 'NONE', #38562, .T. ) ;
#34956=CIRCLE ( 'NONE', #13914, 0.03000000000000008910 ) ;
#34984=DIRECTION ( 'NONE',  ( 1.000000000000000000, 1.138269997360102279E-15, -8.537024980200767584E-16 ) ) ;
#35000=ORIENTED_EDGE ( 'NONE', *, *, #13484, .T. ) ;
#35002=VERTEX_POINT ( 'NONE', #23067 ) ;
#35003=CARTESIAN_POINT ( 'NONE',  ( -0.1210148435730249716, -0.5061394519557976812, 0.3122829191278992389 ) ) ;
#35014=CARTESIAN_POINT ( 'NONE',  ( -0.1529829672178560085, 0.4739133692255316777, 0.09550516375522978552 ) ) ;
#35024=CARTESIAN_POINT ( 'NONE',  ( -0.1664683893528073888, 0.5171715631282249870, 0.3299773601679621415 ) ) ;
#35056=CARTESIAN_POINT ( 'NONE',  ( -0.2666757540196708076, 0.4921670437878968851, 0.3749999999999999445 ) ) ;
#35064=VERTEX_POINT ( 'NONE', #11312 ) ;
#35104=CARTESIAN_POINT ( 'NONE',  ( -0.1593715683900588098, 0.4948507460962289217, 0.3535463917166351555 ) ) ;
#35108=AXIS2_PLACEMENT_3D ( 'NONE', #29912, #4780, #11177 ) ;
#35126=VERTEX_POINT ( 'NONE', #40512 ) ;
#35237=CARTESIAN_POINT ( 'NONE',  ( -0.1574073192761877849, 0.4884966930313972555, 0.1147307106484478645 ) ) ;
#35261=CARTESIAN_POINT ( 'NONE',  ( -0.1873388932668324236, 0.5325605939836577374, 0.09999999999999975575 ) ) ;
#35288=CIRCLE ( 'NONE', #26757, 0.03000000000000029379 ) ;
#35293=CARTESIAN_POINT ( 'NONE',  ( -0.2300000000000000655, 0.5182417262804733804, 0.3749999999999999445 ) ) ;
#35318=DIRECTION ( 'NONE',  ( 1.000000000000000000, 2.276539994720212446E-15, 0.000000000000000000 ) ) ;
#35338=DIRECTION ( 'NONE',  ( -8.881784197001245421E-16, 2.361472542561082612E-16, -1.000000000000000000 ) ) ;
#35539=CARTESIAN_POINT ( 'NONE',  ( -0.1603938765018561030, 0.4636889572247975266, 0.3382895567582887564 ) ) ;
#35550=EDGE_LOOP ( 'NONE', ( #25410, #9092, #26510, #19766 ) ) ;
#35555=B_SPLINE_CURVE_WITH_KNOTS ( 'NONE', 3,
 ( #36908, #15312, #12232, #21086 ),
 .UNSPECIFIED., .F., .F.,
 ( 4, 4 ),
 ( 8.673617379883833249E-19, 0.0003934542678113530680 ),
 .UNSPECIFIED. ) ;
#35615=DIRECTION ( 'NONE',  ( -1.000000000000000000, -2.276539994720197063E-15, 0.000000000000000000 ) ) ;
#35682=EDGE_CURVE ( 'NONE', #5190, #9409, #14711, .T. ) ;
#35762=VERTEX_POINT ( 'NONE', #4498 ) ;
#35791=LINE ( 'NONE', #38063, #21909 ) ;
#35821=ORIENTED_EDGE ( 'NONE', *, *, #39120, .T. ) ;
#35826=CARTESIAN_POINT ( 'NONE',  ( -0.2300000000000000655, 0.5182417262804733804, 0.3749999999999999445 ) ) ;
#35864=CARTESIAN_POINT ( 'NONE',  ( -2.070754768975509919, -0.09959325338431655739, 0.1000000000000005745 ) ) ;
#35865=VERTEX_POINT ( 'NONE', #18227 ) ;
#35879=EDGE_CURVE ( 'NONE', #25455, #29556, #6831, .T. ) ;
#35909=CARTESIAN_POINT ( 'NONE',  ( -2.070754768975509919, -0.09959325338431655739, 0.09813923389047504720 ) ) ;
#35913=CARTESIAN_POINT ( 'NONE',  ( -2.070754768975509474, -0.09959325338431655739, 0.08500000000000142164 ) ) ;
#35930=CARTESIAN_POINT ( 'NONE',  ( -0.1044460467970231704, -0.4741855622371820567, 0.3602693341844405150 ) ) ;
#35989=DIRECTION ( 'NONE',  ( -8.881784197001245421E-16, 2.361472542561082612E-16, -1.000000000000000000 ) ) ;
#36040=CARTESIAN_POINT ( 'NONE',  ( -0.1210148435730035998, -0.5061394519556905447, 0.1438724812234790928 ) ) ;
#36093=CARTESIAN_POINT ( 'NONE',  ( -0.1157923916715204865, -0.5295015842444287246, 0.1380392329925466954 ) ) ;
#36109=CYLINDRICAL_SURFACE ( 'NONE', #13408, 1.991674066779353547 ) ;
#36126=ORIENTED_EDGE ( 'NONE', *, *, #9212, .T. ) ;
#36203=ORIENTED_EDGE ( 'NONE', *, *, #20600, .T. ) ;
#36216=CYLINDRICAL_SURFACE ( 'NONE', #8205, 0.03000000000000029379 ) ;
#36278=AXIS2_PLACEMENT_3D ( 'NONE', #9838, #9223, #34734 ) ;
#36333=EDGE_CURVE ( 'NONE', #35762, #25919, #14397, .T. ) ;
#36362=CIRCLE ( 'NONE', #940, 0.06000000000000045575 ) ;
#36368=EDGE_CURVE ( 'NONE', #36928, #27541, #31844, .T. ) ;
#36434=VERTEX_POINT ( 'NONE', #32331 ) ;
#36435=ORIENTED_EDGE ( 'NONE', *, *, #29541, .F. ) ;
#36451=CARTESIAN_POINT ( 'NONE',  ( -0.1212602504878780296, -0.5073146173917506552, 0.1528658435936999238 ) ) ;
#36510=CARTESIAN_POINT ( 'NONE',  ( -0.1104192559602747703, -0.5043764815743673191, 0.1033498972402037835 ) ) ;
#36577=CARTESIAN_POINT ( 'NONE',  ( -0.1157923916715204865, -0.5295015842444287246, 0.1380392329925466954 ) ) ;
#36587=VERTEX_POINT ( 'NONE', #26980 ) ;
#36595=ORIENTED_EDGE ( 'NONE', *, *, #10148, .T. ) ;
#36628=CARTESIAN_POINT ( 'NONE',  ( -0.1103620673373586075, -0.5040504500050040360, 0.1035024533007080916 ) ) ;
#36645=( BOUNDED_SURFACE ( )  B_SPLINE_SURFACE ( 3, 2, ( 
 ( #30233, #39704, #5325 ),
 ( #15216, #26959, #2676 ),
 ( #2283, #2483, #27772 ),
 ( #21614, #39492, #18107 ),
 ( #11537, #24102, #36628 ),
 ( #8844, #40312, #33733 ),
 ( #8431, #5546, #12141 ),
 ( #20996, #21421, #33954 ),
 ( #30454, #18312, #40096 ),
 ( #14822, #11731, #27387 ) ),
 .UNSPECIFIED., .F., .F., .T. ) 
 B_SPLINE_SURFACE_WITH_KNOTS ( ( 4, 2, 2, 2, 4 ),
 ( 3, 3 ),
 ( 0.001500576079630530895, 0.001976458225352494859, 0.002452340371074459256, 0.002928222516796423220, 0.003404104662518387184 ),
 ( 0.000000000000000000, 1.000000000000000000 ),
 .UNSPECIFIED. ) 
 GEOMETRIC_REPRESENTATION_ITEM ( )  RATIONAL_B_SPLINE_SURFACE ( (
 ( 1.000000000000000000, 0.9128709291753008825, 1.000000000000000000),
 ( 1.000000000000000000, 0.9128711300565840459, 1.000000000000000000),
 ( 1.000000000000000000, 0.9128295461285025336, 1.000000000000000000),
 ( 1.000000000000000000, 0.9126769222979866925, 1.000000000000000000),
 ( 1.000000000000000000, 0.9125696619634834361, 1.000000000000000000),
 ( 1.000000000000000000, 0.9123247991096318232, 1.000000000000000000),
 ( 1.000000000000000000, 0.9121939566646036779, 1.000000000000000000),
 ( 1.000000000000000000, 0.9119567588130496061, 1.000000000000000000),
 ( 1.000000000000000000, 0.9118559517119447788, 1.000000000000000000),
 ( 1.000000000000000000, 0.9117915798251980952, 1.000000000000000000) ) ) 
 REPRESENTATION_ITEM ( '' )  SURFACE ( )  );
#36669=EDGE_CURVE ( 'NONE', #27130, #4891, #4893, .T. ) ;
#36681=ORIENTED_EDGE ( 'NONE', *, *, #15299, .F. ) ;
#36699=DIRECTION ( 'NONE',  ( 1.445848444424219201E-15, -1.000000000000000000, -2.361472542561095431E-16 ) ) ;
#36706=DIRECTION ( 'NONE',  ( 0.3181970600707391683, -0.9480245940703956320, -2.369716614345735130E-16 ) ) ;
#36752=DIRECTION ( 'NONE',  ( 1.000000000000000000, 1.450080480853946466E-15, -8.881784197001242463E-16 ) ) ;
#36791=ADVANCED_FACE ( 'NONE', ( #5299 ), #26542, .T. ) ;
#36832=LINE ( 'NONE', #8043, #13931 ) ;
#36856=ORIENTED_EDGE ( 'NONE', *, *, #17783, .F. ) ;
#36880=ADVANCED_FACE ( 'NONE', ( #11511 ), #12477, .T. ) ;
#36889=CARTESIAN_POINT ( 'NONE',  ( -0.1684323895664678050, 0.5231977504175356897, 0.1528658435937002014 ) ) ;
#36893=DIRECTION ( 'NONE',  ( 1.000000000000000000, 1.138269997360109379E-15, 0.000000000000000000 ) ) ;
#36905=AXIS2_PLACEMENT_3D ( 'NONE', #26253, #19665, #10601 ) ;
#36908=CARTESIAN_POINT ( 'NONE',  ( -0.1167294259372886750, -0.5331983348239501819, 0.3032895567580813356 ) ) ;
#36928=VERTEX_POINT ( 'NONE', #15190 ) ;
#36939=ORIENTED_EDGE ( 'NONE', *, *, #23589, .T. ) ;
#36980=ORIENTED_EDGE ( 'NONE', *, *, #12180, .T. ) ;
#36996=CARTESIAN_POINT ( 'NONE',  ( -0.1154414454259510697, -0.5279056935456387656, 0.3241024189951586254 ) ) ;
#37016=ORIENTED_EDGE ( 'NONE', *, *, #38938, .F. ) ;
#37018=CARTESIAN_POINT ( 'NONE',  ( -0.1044460467970231704, -0.4741855622371820567, 0.3602693341844405150 ) ) ;
#37079=ORIENTED_EDGE ( 'NONE', *, *, #38643, .T. ) ;
#37101=CARTESIAN_POINT ( 'NONE',  ( -0.1339136704200473149, -0.4685718226220191851, 0.3606502365330780946 ) ) ;
#37104=VECTOR ( 'NONE', #33033, 39.37007874015748143 ) ;
#37133=EDGE_CURVE ( 'NONE', #5846, #12135, #32555, .T. ) ;
#37190=ORIENTED_EDGE ( 'NONE', *, *, #30272, .T. ) ;
#37212=CIRCLE ( 'NONE', #39185, 0.03000000000000029379 ) ;
#37223=DIRECTION ( 'NONE',  ( 8.881784197001246407E-16, -2.361472542561082612E-16, 1.000000000000000000 ) ) ;
#37234=DIRECTION ( 'NONE',  ( 0.8150167559926640992, 0.5794373887239191445, -1.138269997360107406E-15 ) ) ;
#37240=B_SPLINE_CURVE_WITH_KNOTS ( 'NONE', 3,
 ( #36451, #14026, #33356, #36040 ),
 .UNSPECIFIED., .F., .F.,
 ( 4, 4 ),
 ( 4.336808689942042773E-19, 0.0002303018524726760570 ),
 .UNSPECIFIED. ) ;
#37300=CARTESIAN_POINT ( 'NONE',  ( -0.08408070219615466911, -0.09959325338431376795, 0.3600000000000005418 ) ) ;
#37313=AXIS2_PLACEMENT_3D ( 'NONE', #5853, #30573, #8749 ) ;
#37314=CARTESIAN_POINT ( 'NONE',  ( -1.019575837292305831, -0.04310840302198155199, 0.3750000000000002220 ) ) ;
#37322=ORIENTED_EDGE ( 'NONE', *, *, #10988, .T. ) ;
#37333=ORIENTED_EDGE ( 'NONE', *, *, #8277, .F. ) ;
#37344=DIRECTION ( 'NONE',  ( 1.000000000000000000, 1.517693329813468127E-15, -1.517693329813468127E-15 ) ) ;
#37372=DIRECTION ( 'NONE',  ( -8.881784197001246407E-16, 2.361472542561082612E-16, -1.000000000000000000 ) ) ;
#37383=ORIENTED_EDGE ( 'NONE', *, *, #23810, .T. ) ;
#37387=FACE_OUTER_BOUND ( 'NONE', #26842, .T. ) ;
#37391=EDGE_CURVE ( 'NONE', #4809, #22283, #40345, .T. ) ;
#37401=CARTESIAN_POINT ( 'NONE',  ( -0.1068374249684430066, -0.4867512985519860114, 0.3606502370888305387 ) ) ;
#37404=DIRECTION ( 'NONE',  ( -0.4887635750372997245, -0.8724162812079783169, 4.149599771362008055E-15 ) ) ;
#37491=CARTESIAN_POINT ( 'NONE',  ( -0.1608542991165662073, 0.4995867522469580324, 0.3503927954982321569 ) ) ;
#37513=ORIENTED_EDGE ( 'NONE', *, *, #28045, .F. ) ;
#37588=EDGE_LOOP ( 'NONE', ( #36203, #17346, #39809, #17137 ) ) ;
#37599=CARTESIAN_POINT ( 'NONE',  ( -0.1157923916715207918, -0.5295015842444125154, 0.3181161673586298533 ) ) ;
#37602=CARTESIAN_POINT ( 'NONE',  ( -0.1157923916715206114, -0.5295015842444287246, 0.1000000000000000194 ) ) ;
#37603=CIRCLE ( 'NONE', #36278, 0.06000000000000045575 ) ;
#37659=APPLICATION_CONTEXT ( 'configuration controlled 3d designs of mechanical parts and assemblies' ) ;
#37700=CARTESIAN_POINT ( 'NONE',  ( -0.1621871387067669035, 0.5037941088976310988, 0.1094562450723023384 ) ) ;
#37722=AXIS2_PLACEMENT_3D ( 'NONE', #35864, #32967, #33182 ) ;
#37751=DIRECTION ( 'NONE',  ( 1.000000000000000000, 2.276539994720212446E-15, -1.138269997360106223E-15 ) ) ;
#37783=EDGE_LOOP ( 'NONE', ( #9252, #27889, #29699, #22392 ) ) ;
#37791=CYLINDRICAL_SURFACE ( 'NONE', #20124, 0.03000000000000008910 ) ;
#37819=CARTESIAN_POINT ( 'NONE',  ( -0.1148620258665538491, -0.5252635219644070652, 0.3299751171063294297 ) ) ;
#37844=EDGE_LOOP ( 'NONE', ( #32633, #14165, #15016, #29316 ) ) ;
#37845=DIRECTION ( 'NONE',  ( 0.8150167559926670968, 0.5794373887239150367, 0.000000000000000000 ) ) ;
#37933=ORIENTED_EDGE ( 'NONE', *, *, #1471, .F. ) ;
#37948=CARTESIAN_POINT ( 'NONE',  ( -0.1743922129835736579, -0.5166151207188712791, 0.1000000000000000194 ) ) ;
#37950=ORIENTED_EDGE ( 'NONE', *, *, #12329, .T. ) ;
#38060=DIRECTION ( 'NONE',  ( 1.000000000000000000, 1.445897915516965072E-15, -8.881784197001242463E-16 ) ) ;
#38063=CARTESIAN_POINT ( 'NONE',  ( -0.1167294259372886056, -0.5331983348239501819, 0.3749999999999996669 ) ) ;
#38069=CARTESIAN_POINT ( 'NONE',  ( -0.1743922129835736579, -0.5166151207188712791, 0.1000000000000000194 ) ) ;
#38077=DIRECTION ( 'NONE',  ( 1.000000000000000000, 1.450080480853946466E-15, -8.188689774234050758E-16 ) ) ;
#38100=CARTESIAN_POINT ( 'NONE',  ( -0.1683868308082382692, 0.4901225108767979788, 0.1298109267597956917 ) ) ;
#38116=DIRECTION ( 'NONE',  ( -1.000000000000000000, -2.276539994720197063E-15, 5.691349986800492658E-16 ) ) ;
#38258=DIRECTION ( 'NONE',  ( 8.881784197001246407E-16, -2.361472542561082612E-16, 1.000000000000000000 ) ) ;
#38299=FACE_OUTER_BOUND ( 'NONE', #29490, .T. ) ;
#38351=ORIENTED_EDGE ( 'NONE', *, *, #10988, .F. ) ;
#38362=VECTOR ( 'NONE', #13877, 39.37007874015748143 ) ;
#38374=EDGE_CURVE ( 'NONE', #33923, #10991, #23413, .T. ) ;
#38390=ORIENTED_EDGE ( 'NONE', *, *, #14499, .T. ) ;
#38428=CARTESIAN_POINT ( 'NONE',  ( -0.1743922129835736579, -0.5166151207188712791, 0.1000000000000000194 ) ) ;
#38429=AXIS2_PLACEMENT_3D ( 'NONE', #16985, #4606, #33614 ) ;
#38444=CARTESIAN_POINT ( 'NONE',  ( -0.1157923916715200702, -0.5295015842444287246, 0.3181161673586325178 ) ) ;
#38498=ORIENTED_EDGE ( 'NONE', *, *, #13242, .F. ) ;
#38499=EDGE_CURVE ( 'NONE', #1427, #21489, #12222, .T. ) ;
#38562=EDGE_LOOP ( 'NONE', ( #11238, #12438 ) ) ;
#38643=EDGE_CURVE ( 'NONE', #35126, #23460, #40469, .T. ) ;
#38706=DIRECTION ( 'NONE',  ( 1.000000000000000000, 1.450080480853946466E-15, -8.881784197001242463E-16 ) ) ;
#38715=DIRECTION ( 'NONE',  ( 8.881784197001246407E-16, -2.361472542561082612E-16, 1.000000000000000000 ) ) ;
#38856=FACE_OUTER_BOUND ( 'NONE', #37844, .T. ) ;
#38883=CARTESIAN_POINT ( 'NONE',  ( -0.09579104668929012967, -0.04310840302198021973, 0.3599999999999992095 ) ) ;
#38884=ADVANCED_FACE ( 'NONE', ( #39381 ), #20135, .T. ) ;
#38889=ORIENTED_EDGE ( 'NONE', *, *, #20957, .T. ) ;
#38919=( LENGTH_UNIT ( ) NAMED_UNIT ( * ) SI_UNIT ( $, .METRE. ) );
#38938=EDGE_CURVE ( 'NONE', #2775, #30856, #1648, .T. ) ;
#38957=CIRCLE ( 'NONE', #40280, 0.06000000000000045575 ) ;
#38985=AXIS2_PLACEMENT_3D ( 'NONE', #37300, #36699, #36893 ) ;
#39032=CARTESIAN_POINT ( 'NONE',  ( -0.1163452666695150850, -0.5320157244525763884, 0.3133290949223796473 ) ) ;
#39051=CARTESIAN_POINT ( 'NONE',  ( -0.1167294259372882170, -0.5331983348239496268, 0.1476740372344552410 ) ) ;
#39101=ORIENTED_EDGE ( 'NONE', *, *, #29541, .T. ) ;
#39120=EDGE_CURVE ( 'NONE', #25611, #1427, #8955, .T. ) ;
#39124=EDGE_CURVE ( 'NONE', #24171, #3794, #1147, .T. ) ;
#39131=DIRECTION ( 'NONE',  ( -8.881784197001246407E-16, 2.361472542561082612E-16, -1.000000000000000000 ) ) ;
#39165=ORIENTED_EDGE ( 'NONE', *, *, #20057, .T. ) ;
#39185=AXIS2_PLACEMENT_3D ( 'NONE', #22118, #9936, #38116 ) ;
#39194=CARTESIAN_POINT ( 'NONE',  ( -0.1142976700078457836, -0.5226524673290442458, 0.1219895833617486020 ) ) ;
#39220=EDGE_CURVE ( 'NONE', #4891, #27130, #37212, .T. ) ;
#39264=ORIENTED_EDGE ( 'NONE', *, *, #1206, .T. ) ;
#39276=CARTESIAN_POINT ( 'NONE',  ( -0.1574377185082707353, 0.4885537809602767401, 0.1000000000000000194 ) ) ;
#39288=AXIS2_PLACEMENT_3D ( 'NONE', #29096, #15946, #22150 ) ;
#39289=PRODUCT_DEFINITION_CONTEXT ( 'detailed design', #39759, 'design' ) ;
#39322=DIRECTION ( 'NONE',  ( -1.000000000000000000, -1.450080480853946466E-15, 8.188689774234050758E-16 ) ) ;
#39381=FACE_OUTER_BOUND ( 'NONE', #21088, .T. ) ;
#39392=CARTESIAN_POINT ( 'NONE',  ( -0.1157923916715206808, -0.5295015842444287246, 0.3749999999999999445 ) ) ;
#39492=CARTESIAN_POINT ( 'NONE',  ( -0.1081053389376798041, -0.4929871184167937126, 0.1128267017629384777 ) ) ;
#39511=( BOUNDED_SURFACE ( )  B_SPLINE_SURFACE ( 3, 2, ( 
 ( #29533, #19485, #10219 ),
 ( #16799, #29347, #16584 ),
 ( #13882, #7100, #991 ),
 ( #4433, #31818, #35104 ),
 ( #6909, #4020, #32014 ),
 ( #7297, #16992, #1375 ),
 ( #23401, #3823, #19669 ),
 ( #16198, #25649, #32410 ),
 ( #10003, #16380, #26071 ),
 ( #22577, #28920, #22788 ),
 ( #26456, #13692, #26259 ),
 ( #4233, #32623, #25864 ) ),
 .UNSPECIFIED., .F., .F., .T. ) 
 B_SPLINE_SURFACE_WITH_KNOTS ( ( 4, 2, 2, 2, 2, 4 ),
 ( 3, 3 ),
 ( 0.001713391272003884783, 0.002288612648294801721, 0.002863834024585718441, 0.003151444712731176802, 0.003439055400876635596, 0.004014276777167552317 ),
 ( 0.000000000000000000, 1.000000000000000000 ),
 .UNSPECIFIED. ) 
 GEOMETRIC_REPRESENTATION_ITEM ( )  RATIONAL_B_SPLINE_SURFACE ( (
 ( 1.000000000000000000, 0.9128709291753012156, 1.000000000000000000),
 ( 1.000000000000000000, 0.9128719127418516432, 1.000000000000000000),
 ( 1.000000000000000000, 0.9128123349203235426, 1.000000000000000000),
 ( 1.000000000000000000, 0.9126095266096564407, 1.000000000000000000),
 ( 1.000000000000000000, 0.9124632789547948430, 1.000000000000000000),
 ( 1.000000000000000000, 0.9122369551430161705, 1.000000000000000000),
 ( 1.000000000000000000, 0.9121592698944235300, 1.000000000000000000),
 ( 1.000000000000000000, 0.9120159902105161587, 1.000000000000000000),
 ( 1.000000000000000000, 0.9119497308970357929, 1.000000000000000000),
 ( 1.000000000000000000, 0.9117802546605157099, 1.000000000000000000),
 ( 1.000000000000000000, 0.9117114107497396036, 1.000000000000000000),
 ( 1.000000000000000000, 0.9117127123830639501, 1.000000000000000000) ) ) 
 REPRESENTATION_ITEM ( '' )  SURFACE ( )  );
#39515=CIRCLE ( 'NONE', #36905, 0.03000000000000008910 ) ;
#39557=CARTESIAN_POINT ( 'NONE',  ( -2.070754768975509919, -0.09959325338431655739, 0.1178658435937004478 ) ) ;
#39561=EDGE_CURVE ( 'NONE', #36434, #27541, #17704, .T. ) ;
#39566=DIRECTION ( 'NONE',  ( 0.9823333030490233320, -0.1871397384865000069, 0.000000000000000000 ) ) ;
#39660=AXIS2_PLACEMENT_3D ( 'NONE', #30336, #2166, #39799 ) ;
#39675=EDGE_CURVE ( 'NONE', #8795, #5190, #18177, .T. ) ;
#39704=CARTESIAN_POINT ( 'NONE',  ( -0.1044436713285761403, -0.4741860147765892819, 0.1089215716836983705 ) ) ;
#39759=APPLICATION_CONTEXT ( 'configuration controlled 3d designs of mechanical parts and assemblies' ) ;
#39799=DIRECTION ( 'NONE',  ( 1.000000000000000000, 1.450082232674701412E-15, -8.188699666868902382E-16 ) ) ;
#39805=AXIS2_PLACEMENT_3D ( 'NONE', #31477, #853, #7168 ) ;
#39809=ORIENTED_EDGE ( 'NONE', *, *, #2110, .F. ) ;
#39810=CARTESIAN_POINT ( 'NONE',  ( -0.1129900121204594904, -0.5167580615068187999, 0.1415474730880565690 ) ) ;
#39838=CARTESIAN_POINT ( 'NONE',  ( -0.1522836376793811619, 0.4715211068759145308, 0.3601997132473424568 ) ) ;
#39928=VERTEX_POINT ( 'NONE', #30478 ) ;
#39961=ORIENTED_EDGE ( 'NONE', *, *, #13141, .F. ) ;
#39967=ORIENTED_EDGE ( 'NONE', *, *, #18481, .F. ) ;
#40023=CARTESIAN_POINT ( 'NONE',  ( -0.1088121136105144049, -0.4964308608213456875, 0.1000000000000000194 ) ) ;
#40031=CARTESIAN_POINT ( 'NONE',  ( -0.1667650433730323567, 0.4848728453260168769, 0.3315300532330299199 ) ) ;
#40073=CARTESIAN_POINT ( 'NONE',  ( -0.1208133668958207424, -0.5051731972035693463, 0.3159170889047836495 ) ) ;
#40093=CARTESIAN_POINT ( 'NONE',  ( -0.1055448275397422725, -0.4799318856336941552, 0.3601683063145876273 ) ) ;
#40096=CARTESIAN_POINT ( 'NONE',  ( -0.1154362047091238019, -0.5278818619436607129, 0.1319635891398989735 ) ) ;
#40231=CARTESIAN_POINT ( 'NONE',  ( -0.1530296545635674021, 0.4740172026173952724, 0.3600612075995240913 ) ) ;
#40243=AXIS2_PLACEMENT_3D ( 'NONE', #8835, #5318, #11918 ) ;
#40253=DIRECTION ( 'NONE',  ( 1.000000000000000000, 1.448788479720436075E-15, -8.229804381843896237E-16 ) ) ;
#40273=ORIENTED_EDGE ( 'NONE', *, *, #20957, .F. ) ;
#40280=AXIS2_PLACEMENT_3D ( 'NONE', #24692, #37223, #9041 ) ;
#40308=VERTEX_POINT ( 'NONE', #12457 ) ;
#40309=CARTESIAN_POINT ( 'NONE',  ( -0.1455608194604306738, -0.5249067277714107860, 0.3749999999999996669 ) ) ;
#40312=CARTESIAN_POINT ( 'NONE',  ( -0.1105199412302043521, -0.5049077968913552317, 0.1209919789212128283 ) ) ;
#40345=B_SPLINE_CURVE_WITH_KNOTS ( 'NONE', 3,
 ( #11850, #15746, #39838, #40231, #11661, #24220, #24417 ),
 .UNSPECIFIED., .F., .F.,
 ( 4, 3, 4 ),
 ( 0.000000000000000000, 0.0001987961317490854899, 0.0002262042107145686282 ),
 .UNSPECIFIED. ) ;
#40368=ORIENTED_EDGE ( 'NONE', *, *, #17783, .T. ) ;
#40370=AXIS2_PLACEMENT_3D ( 'NONE', #6085, #28125, #18655 ) ;
#40399=AXIS2_PLACEMENT_3D ( 'NONE', #35909, #26669, #7718 ) ;
#40453=CARTESIAN_POINT ( 'NONE',  ( -0.1710642718812883378, 0.4986889572247745761, 0.3079501053856181780 ) ) ;
#40469=CIRCLE ( 'NONE', #28001, 0.03000000000000029379 ) ;
#40499=AXIS2_PLACEMENT_3D ( 'NONE', #10808, #20275, #14477 ) ;
#40502=DIRECTION ( 'NONE',  ( 0.8724162812079789830, -0.4887635750372981702, 0.000000000000000000 ) ) ;
#40512=CARTESIAN_POINT ( 'NONE',  ( -0.1999999999999998446, 0.5182417262804734914, 0.3749999999999999445 ) ) ;
#40582=CARTESIAN_POINT ( 'NONE',  ( -0.1684323895664760207, 0.5231977504175434612, 0.1528658435937284565 ) ) ;
#40607=CARTESIAN_POINT ( 'NONE',  ( -0.1212602504878817211, -0.5073146173917503221, 0.3048175120576748220 ) ) ;
#40681=COLOUR_RGB('Sky Blue',0.24,0.69,0.87);
#40682=FILL_AREA_STYLE_COLOUR('',#40681);
#40683=FILL_AREA_STYLE('',(#40682));
#40684=SURFACE_STYLE_FILL_AREA(#40683);
#40685=SURFACE_SIDE_STYLE('',(#40684));
#40686=SURFACE_STYLE_USAGE(.BOTH.,#40685);
#40687=PRESENTATION_STYLE_ASSIGNMENT((#40686));
#40715=STYLED_ITEM('',(#40687),#19057);
#40721=MECHANICAL_DESIGN_GEOMETRIC_PRESENTATION_REPRESENTATION('',(#40715),#11399);
ENDSEC;
END-ISO-10303-21;
